ISO-10303-21;
HEADER;
FILE_DESCRIPTION (('STEP AP214'),
    '1' );
FILE_NAME ('hex flange nut gradea_iso_ISO - 4161 - M5 - N.step',
    '2026-10-27T17:01:19',
    ( '' ),
    ( '' ),
    'SwSTEP 2.0',
    'SolidWorks 2026',
    '' );
FILE_SCHEMA (( 'AUTOMOTIVE_DESIGN' ));
ENDSEC;

DATA;
#5=ORIENTED_EDGE ( 'NONE', *, *, #10243, .F. ) ;
#43=DIRECTION ( 'NONE',  ( 0.000000000000000000, 0.000000000000000000, -1.000000000000000000 ) ) ;
#51=STYLED_ITEM('',(#14681),#12291);
#69=CARTESIAN_POINT ( 'NONE',  ( -3.511755186886750479, 2.826662030176366081, -3.597382984111578086 ) ) ;
#71=CARTESIAN_POINT ( 'NONE',  ( -4.197393957002303999, 0.4069871074557429025, -3.503767560748926257 ) ) ;
#88=EDGE_CURVE ( 'NONE', #5056, #3419, #11622, .T. ) ;
#92=CARTESIAN_POINT ( 'NONE',  ( 2.500000000000000888, 3.061616997868384127E-16, -4.974599999999998801 ) ) ;
#112=CARTESIAN_POINT ( 'NONE',  ( 0.000000000000000000, 0.000000000000000000, -4.974599999999998801 ) ) ;
#154=ORIENTED_EDGE ( 'NONE', *, *, #12359, .F. ) ;
#155=CARTESIAN_POINT ( 'NONE',  ( -6.259644161404860030E-16, -4.618802153517027165, -5.000000000000000000 ) ) ;
#163=DIRECTION ( 'NONE',  ( 1.000000000000000000, 0.000000000000000000, 0.000000000000000000 ) ) ;
#170=CARTESIAN_POINT ( 'NONE',  ( 0.6507732100473444525, -4.243078065514795050, -0.2236248678334952777 ) ) ;
#186=EDGE_CURVE ( 'NONE', #3815, #10556, #4083, .T. ) ;
#212=VECTOR ( 'NONE', #12362, 1000.000000000000000 ) ;
#278=CARTESIAN_POINT ( 'NONE',  ( 4.000000000000000000, -2.309401076758514915, -3.433295621305383349 ) ) ;
#307=CARTESIAN_POINT ( 'NONE',  ( -0.1404048886732797152, -4.699864953788083888, -3.686887068327043160 ) ) ;
#316=CARTESIAN_POINT ( 'NONE',  ( 1.391697335622810172, 4.043246145443375461, -3.503898532754365913 ) ) ;
#332=ORIENTED_EDGE ( 'NONE', *, *, #5036, .F. ) ;
#362=DIRECTION ( 'NONE',  ( -0.8191520442889902442, 0.000000000000000000, -0.5735764363510482688 ) ) ;
#405=CARTESIAN_POINT ( 'NONE',  ( 1.567478505476134606E-15, 4.618802153517012066, -3.433295621305382905 ) ) ;
#415=CARTESIAN_POINT ( 'NONE',  ( -4.000000000000000000, 0.8730739991738342143, -3.223134629628428893 ) ) ;
#422=ORIENTED_EDGE ( 'NONE', *, *, #7911, .F. ) ;
#449=FACE_OUTER_BOUND ( 'NONE', #2353, .T. ) ;
#477=CARTESIAN_POINT ( 'NONE',  ( 1.411581201560190495E-15, 4.862606272033091592, -3.745885042887436622 ) ) ;
#502=DIRECTION ( 'NONE',  ( -1.000000000000000000, 0.000000000000000000, 0.000000000000000000 ) ) ;
#513=CARTESIAN_POINT ( 'NONE',  ( 4.000000000000000000, 2.512223110932545023, -3.469391141908803711 ) ) ;
#560=ORIENTED_EDGE ( 'NONE', *, *, #3377, .F. ) ;
#568=CARTESIAN_POINT ( 'NONE',  ( 1.274258131564866448, 3.883108878240963513, -3.220599429844046568 ) ) ;
#570=CARTESIAN_POINT ( 'NONE',  ( -4.197312064133472020, -0.8182229787990021874, -3.502518405183886685 ) ) ;
#578=B_SPLINE_CURVE_WITH_KNOTS ( 'NONE', 3,
 ( #828, #8746, #7644, #8878, #7706, #2012, #6527, #11020 ),
 .UNSPECIFIED., .F., .F.,
 ( 4, 2, 2, 4 ),
 ( 2.465131517071352357E-07, 0.001183067374689843057, 0.001774477805458910071, 0.002365888236227977302 ),
 .UNSPECIFIED. ) ;
#614=CARTESIAN_POINT ( 'NONE',  ( 0.000000000000000000, 0.000000000000000000, 3.469446951953614189E-15 ) ) ;
#637=CARTESIAN_POINT ( 'NONE',  ( -4.000000000000000000, -2.512220745329312610, -3.469390707569719901 ) ) ;
#658=EDGE_LOOP ( 'NONE', ( #9562, #1387, #14345, #2712 ) ) ;
#670=AXIS2_PLACEMENT_3D ( 'NONE', #13572, #3196, #13733 ) ;
#672=CARTESIAN_POINT ( 'NONE',  ( 8.673617379884035472E-16, 4.618802153517012954, 0.000000000000000000 ) ) ;
#680=ORIENTED_EDGE ( 'NONE', *, *, #186, .T. ) ;
#710=CARTESIAN_POINT ( 'NONE',  ( 0.000000000000000000, 0.000000000000000000, -4.484454397937119197 ) ) ;
#720=ORIENTED_EDGE ( 'NONE', *, *, #6916, .T. ) ;
#740=VERTEX_POINT ( 'NONE', #866 ) ;
#742=CARTESIAN_POINT ( 'NONE',  ( -4.000000000000000000, -2.309401076758512694, -5.000000000000000000 ) ) ;
#749=DIRECTION ( 'NONE',  ( 1.000000000000000000, 0.000000000000000000, 0.000000000000000000 ) ) ;
#751=AXIS2_PLACEMENT_3D ( 'NONE', #10537, #4872, #13863 ) ;
#756=DIRECTION ( 'NONE',  ( 1.000000000000000000, 0.000000000000000000, 0.000000000000000000 ) ) ;
#765=B_SPLINE_CURVE_WITH_KNOTS ( 'NONE', 3,
 ( #2758, #11683, #13033, #2695, #5129, #10670, #8434, #11837 ),
 .UNSPECIFIED., .F., .F.,
 ( 4, 2, 2, 4 ),
 ( 0.005725059856848641743, 0.006314084072593626612, 0.006903108288338611481, 0.008081156719828581220 ),
 .UNSPECIFIED. ) ;
#773=CARTESIAN_POINT ( 'NONE',  ( 0.1410422978106145031, -4.700232962125109104, -3.687027686973628704 ) ) ;
#784=DIRECTION ( 'NONE',  ( 1.000000000000000000, 0.000000000000000000, 0.000000000000000000 ) ) ;
#828=CARTESIAN_POINT ( 'NONE',  ( -4.000000000000000000, 2.309401076758498483, -0.4999999999999927280 ) ) ;
#856=ADVANCED_FACE ( 'NONE', ( #9003 ), #4603, .F. ) ;
#866=CARTESIAN_POINT ( 'NONE',  ( 2.000000000000005329, -3.464101615137751722, 0.000000000000000000 ) ) ;
#890=DIRECTION ( 'NONE',  ( 0.000000000000000000, 0.000000000000000000, -1.000000000000000000 ) ) ;
#900=FACE_OUTER_BOUND ( 'NONE', #12459, .T. ) ;
#908=CARTESIAN_POINT ( 'NONE',  ( -1.360585162435467455, 4.061296242128285883, -3.505054077164959203 ) ) ;
#921=DIRECTION ( 'NONE',  ( -1.000000000000000000, 0.000000000000000000, 0.000000000000000000 ) ) ;
#923=ORIENTED_EDGE ( 'NONE', *, *, #7288, .F. ) ;
#924=CARTESIAN_POINT ( 'NONE',  ( 3.355112389629172576, -2.681727112203168950, -0.2256878752776777242 ) ) ;
#934=FACE_OUTER_BOUND ( 'NONE', #4769, .T. ) ;
#965=ORIENTED_EDGE ( 'NONE', *, *, #10253, .F. ) ;
#968=B_SPLINE_CURVE_WITH_KNOTS ( 'NONE', 3,
 ( #12277, #12352, #6819, #1286, #11322 ),
 .UNSPECIFIED., .F., .F.,
 ( 4, 1, 4 ),
 ( 5.640274452250024914E-20, 0.002309401076758505356, 0.004618802153517010713 ),
 .UNSPECIFIED. ) ;
#978=ORIENTED_EDGE ( 'NONE', *, *, #4982, .T. ) ;
#987=CARTESIAN_POINT ( 'NONE',  ( 0.3198814748697593746, 4.434118497892183264, -0.3507732604232499107 ) ) ;
#992=VERTEX_POINT ( 'NONE', #13950 ) ;
#998=ADVANCED_FACE ( 'NONE', ( #12835, #2716 ), #2570, .T. ) ;
#1001=CARTESIAN_POINT ( 'NONE',  ( -2.500000000000000444, 3.061616997868383634E-16, -25.03750572909317285 ) ) ;
#1022=APPLICATION_CONTEXT ( 'automotive_design' ) ;
#1056=CARTESIAN_POINT ( 'NONE',  ( -1.655952806101422814, 3.662737355149034979, -7.623296525288699970E-18 ) ) ;
#1069=LINE ( 'NONE', #1001, #212 ) ;
#1070=CARTESIAN_POINT ( 'NONE',  ( 0.000000000000000000, 0.000000000000000000, -4.694516984716113228 ) ) ;
#1080=DIRECTION ( 'NONE',  ( 0.8191520442889875797, 0.000000000000000000, 0.5735764363510522656 ) ) ;
#1082=EDGE_LOOP ( 'NONE', ( #12851, #11532 ) ) ;
#1100=ADVANCED_FACE ( 'NONE', ( #1755 ), #2999, .F. ) ;
#1107=CARTESIAN_POINT ( 'NONE',  ( 1.567478505476134606E-15, 4.618802153517012066, -3.433295621305382905 ) ) ;
#1113=CARTESIAN_POINT ( 'NONE',  ( 4.197393957002303999, -0.4069871074557456780, -3.503767560748925813 ) ) ;
#1153=B_SPLINE_CURVE_WITH_KNOTS ( 'NONE', 3,
 ( #6799, #13590, #8056, #7914, #10271 ),
 .UNSPECIFIED., .F., .F.,
 ( 4, 1, 4 ),
 ( 0.000000000000000000, 0.002309401076758505790, 0.004618802153517011580 ),
 .UNSPECIFIED. ) ;
#1161=CARTESIAN_POINT ( 'NONE',  ( 3.999999999999999112, -0.3979232138631231819, -5.929230630780099908E-17 ) ) ;
#1177=ORIENTED_EDGE ( 'NONE', *, *, #3606, .F. ) ;
#1200=CIRCLE ( 'NONE', #13231, 2.100000000000000089 ) ;
#1202=CARTESIAN_POINT ( 'NONE',  ( -4.198928548860774157, 0.8158838809860065044, -3.526471437616918170 ) ) ;
#1203=EDGE_LOOP ( 'NONE', ( #10875, #5229, #6450, #4248, #6568 ) ) ;
#1207=CARTESIAN_POINT ( 'NONE',  ( 1.144235203016666258, 3.958177651039090250, -0.09382832055445661235 ) ) ;
#1238=VERTEX_POINT ( 'NONE', #2976 ) ;
#1240=EDGE_LOOP ( 'NONE', ( #11426, #3550, #720, #5987 ) ) ;
#1250=AXIS2_PLACEMENT_3D ( 'NONE', #11877, #11805, #10705 ) ;
#1253=B_SPLINE_CURVE_WITH_KNOTS ( 'NONE', 3,
 ( #6029, #10242, #10312, #9289, #3681, #8161 ),
 .UNSPECIFIED., .F., .F.,
 ( 4, 2, 4 ),
 ( 0.003358874760055550156, 0.004541967308452096383, 0.005725059856848641743 ),
 .UNSPECIFIED. ) ;
#1263=ORIENTED_EDGE ( 'NONE', *, *, #6739, .F. ) ;
#1280=CARTESIAN_POINT ( 'NONE',  ( 4.000000000000000000, -0.8732470631449981147, -3.223155494240760088 ) ) ;
#1284=CARTESIAN_POINT ( 'NONE',  ( 0.000000000000000000, 0.000000000000000000, -0.2800830152838844622 ) ) ;
#1286=CARTESIAN_POINT ( 'NONE',  ( 3.333333333333335702, -2.694301256218268215, -3.300726591567084256 ) ) ;
#1334=ADVANCED_FACE ( 'NONE', ( #8292, #6291 ), #9555, .F. ) ;
#1367=AXIS2_PLACEMENT_3D ( 'NONE', #672, #13093, #8512 ) ;
#1369=DIRECTION ( 'NONE',  ( 0.000000000000000000, 0.000000000000000000, 1.000000000000000000 ) ) ;
#1371=VERTEX_POINT ( 'NONE', #13022 ) ;
#1387=ORIENTED_EDGE ( 'NONE', *, *, #2488, .T. ) ;
#1396=CARTESIAN_POINT ( 'NONE',  ( 4.197393957002303999, 7.772902908466098641E-14, -3.503767560748929810 ) ) ;
#1417=ORIENTED_EDGE ( 'NONE', *, *, #6202, .F. ) ;
#1427=ORIENTED_EDGE ( 'NONE', *, *, #7911, .T. ) ;
#1433=DIRECTION ( 'NONE',  ( 0.000000000000000000, 0.000000000000000000, 1.000000000000000000 ) ) ;
#1441=ORIENTED_EDGE ( 'NONE', *, *, #13691, .T. ) ;
#1449=DIRECTION ( 'NONE',  ( -0.000000000000000000, -0.000000000000000000, 1.000000000000000000 ) ) ;
#1491=CARTESIAN_POINT ( 'NONE',  ( -1.144235203016679359, -3.958177651039096911, -0.09382832055446428676 ) ) ;
#1511=CARTESIAN_POINT ( 'NONE',  ( 2.712762565639649015, -3.052587955997662306, -3.430618716626630871 ) ) ;
#1518=DIRECTION ( 'NONE',  ( 0.000000000000000000, 0.000000000000000000, 1.000000000000000000 ) ) ;
#1529=CARTESIAN_POINT ( 'NONE',  ( 4.154306624730864428, 2.398490048084778170, -3.721999068284300272 ) ) ;
#1537=CARTESIAN_POINT ( 'NONE',  ( 0.5636800770130377947, 4.293361309317166530, -3.531542292954102713 ) ) ;
#1542=CARTESIAN_POINT ( 'NONE',  ( 2.499999999999999556, 0.000000000000000000, 3.469446951953614189E-15 ) ) ;
#1568=CARTESIAN_POINT ( 'NONE',  ( 2.100000000000000089, 0.000000000000000000, -5.000000000000000000 ) ) ;
#1630=VERTEX_POINT ( 'NONE', #1107 ) ;
#1634=B_SPLINE_CURVE_WITH_KNOTS ( 'NONE', 3,
 ( #8242, #12755, #2648, #7146, #405 ),
 .UNSPECIFIED., .F., .F.,
 ( 4, 1, 4 ),
 ( 0.000000000000000000, 0.002309401076758505356, 0.004618802153517010713 ),
 .UNSPECIFIED. ) ;
#1637=AXIS2_PLACEMENT_3D ( 'NONE', #10873, #6285, #749 ) ;
#1639=CYLINDRICAL_SURFACE ( 'NONE', #1637, 2.500000000000000444 ) ;
#1646=AXIS2_PLACEMENT_3D ( 'NONE', #12884, #2769, #9346 ) ;
#1653=CARTESIAN_POINT ( 'NONE',  ( 3.436319922986518449, -2.634841920959471562, -3.531542292954761741 ) ) ;
#1660=VECTOR ( 'NONE', #1433, 1000.000000000000000 ) ;
#1667=EDGE_CURVE ( 'NONE', #3851, #9996, #1153, .T. ) ;
#1692=CARTESIAN_POINT ( 'NONE',  ( -0.1410422978106123659, 4.700232962125094893, -3.687027686973624707 ) ) ;
#1700=ADVANCED_FACE ( 'NONE', ( #4672 ), #3415, .T. ) ;
#1740=DIRECTION ( 'NONE',  ( 0.000000000000000000, 0.000000000000000000, -1.000000000000000000 ) ) ;
#1754=CARTESIAN_POINT ( 'NONE',  ( 4.000000000000000000, 2.309401076758515803, -0.4999999999999995559 ) ) ;
#1755=FACE_OUTER_BOUND ( 'NONE', #3068, .T. ) ;
#1757=ORIENTED_EDGE ( 'NONE', *, *, #9309, .F. ) ;
#1778=CARTESIAN_POINT ( 'NONE',  ( -5.560781378645573980, 0.000000000000000000, -4.000000000000000000 ) ) ;
#1806=EDGE_LOOP ( 'NONE', ( #10812, #11402, #13673 ) ) ;
#1827=ORIENTED_EDGE ( 'NONE', *, *, #4130, .F. ) ;
#1854=ORIENTED_EDGE ( 'NONE', *, *, #10722, .F. ) ;
#1856=CARTESIAN_POINT ( 'NONE',  ( 4.000000000000000888, 1.563622288139206118, -0.2253451193528334950 ) ) ;
#1857=DIRECTION ( 'NONE',  ( -1.000000000000000000, 0.000000000000000000, 0.000000000000000000 ) ) ;
#1880=VERTEX_POINT ( 'NONE', #10931 ) ;
#1894=CONICAL_SURFACE ( 'NONE', #2838, 2.500000000000000888, 0.9599310885968785900 ) ;
#1905=EDGE_LOOP ( 'NONE', ( #2174, #8731, #3580, #11453 ) ) ;
#1947=CARTESIAN_POINT ( 'NONE',  ( -4.000000000000000000, -2.309401076758512694, -3.433295621305382461 ) ) ;
#1960=CARTESIAN_POINT ( 'NONE',  ( -0.5449313310646672903, -4.304185902836978883, -3.316620875263469159 ) ) ;
#1963=MECHANICAL_DESIGN_GEOMETRIC_PRESENTATION_REPRESENTATION('',(#51),#14000);
#1983=APPLICATION_CONTEXT ( 'automotive_design' ) ;
#2012=CARTESIAN_POINT ( 'NONE',  ( -2.345747346278108214, 3.264484291692489215, -0.01223254789873409049 ) ) ;
#2026=ORIENTED_EDGE ( 'NONE', *, *, #3707, .F. ) ;
#2028=EDGE_CURVE ( 'NONE', #10838, #1371, #12662, .T. ) ;
#2036=ORIENTED_EDGE ( 'NONE', *, *, #6739, .T. ) ;
#2037=B_SPLINE_CURVE_WITH_KNOTS ( 'NONE', 3,
 ( #3723, #8207, #12717, #2615, #10793, #14119 ),
 .UNSPECIFIED., .F., .F.,
 ( 4, 2, 4 ),
 ( 0.000000000000000000, 0.0002095117440864791795, 0.0004190234881729583589 ),
 .UNSPECIFIED. ) ;
#2090=CARTESIAN_POINT ( 'NONE',  ( -2.499999999999999556, 3.061616997868382648E-16, 3.469446951953614189E-15 ) ) ;
#2105=DIRECTION ( 'NONE',  ( 0.8191520442889902442, 1.003171929053522651E-16, -0.5735764363510482688 ) ) ;
#2114=CIRCLE ( 'NONE', #6136, 2.500000000000000888 ) ;
#2115=PLANE ( 'NONE',  #2547 ) ;
#2119=CARTESIAN_POINT ( 'NONE',  ( 4.000000000000000000, -2.309401076758516691, -0.4999999999999995559 ) ) ;
#2159=( GEOMETRIC_REPRESENTATION_CONTEXT ( 3 ) GLOBAL_UNCERTAINTY_ASSIGNED_CONTEXT ( ( #2667 ) ) GLOBAL_UNIT_ASSIGNED_CONTEXT ( ( #14207, #11009, #13162 ) ) REPRESENTATION_CONTEXT ( 'NONE', 'WORKASPACE' ) );
#2162=CARTESIAN_POINT ( 'NONE',  ( -2.100000000000000089, 2.571758278209441957E-16, -0.2800830152838844622 ) ) ;
#2174=ORIENTED_EDGE ( 'NONE', *, *, #4397, .F. ) ;
#2178=ORIENTED_EDGE ( 'NONE', *, *, #14231, .F. ) ;
#2180=FACE_OUTER_BOUND ( 'NONE', #10813, .T. ) ;
#2208=CARTESIAN_POINT ( 'NONE',  ( -2.059999999999998721, 2.522772406243545965E-16, -0.3080913168122742518 ) ) ;
#2209=EDGE_LOOP ( 'NONE', ( #9368, #6756, #10801, #13263, #4741 ) ) ;
#2235=CARTESIAN_POINT ( 'NONE',  ( 1.654252653721905331, 3.663718938583014229, -0.01223254789873410957 ) ) ;
#2236=CARTESIAN_POINT ( 'NONE',  ( 0.1404048886732821022, 4.699864953788070565, -3.686887068327037387 ) ) ;
#2238=( NAMED_UNIT ( * ) PLANE_ANGLE_UNIT ( ) SI_UNIT ( $, .RADIAN. ) );
#2280=ADVANCED_FACE ( 'NONE', ( #6175 ), #3739, .F. ) ;
#2290=VERTEX_POINT ( 'NONE', #2764 ) ;
#2299=ORIENTED_EDGE ( 'NONE', *, *, #8745, .T. ) ;
#2314=VERTEX_POINT ( 'NONE', #4851 ) ;
#2326=CARTESIAN_POINT ( 'NONE',  ( -2.688821387764050996E-14, -4.618802153517012954, -0.4999999999999995559 ) ) ;
#2331=ORIENTED_EDGE ( 'NONE', *, *, #11098, .T. ) ;
#2333=TOROIDAL_SURFACE ( 'NONE', #12469, 5.384454397937118664, 0.5155456020628804703 ) ;
#2345=CONICAL_SURFACE ( 'NONE', #12249, 2.500000000000000888, 0.9599310885968785900 ) ;
#2353=EDGE_LOOP ( 'NONE', ( #10857, #13525, #680, #9937 ) ) ;
#2356=B_SPLINE_CURVE_WITH_KNOTS ( 'NONE', 3,
 ( #4320, #69, #4610, #3355, #11234, #3420, #6886, #7920 ),
 .UNSPECIFIED., .F., .F.,
 ( 4, 2, 2, 4 ),
 ( 0.000000000000000000, 0.002450665683189820997, 0.003675998524784731495, 0.004901331366379641993 ),
 .UNSPECIFIED. ) ;
#2361=AXIS2_PLACEMENT_3D ( 'NONE', #13330, #11036, #921 ) ;
#2364=CARTESIAN_POINT ( 'NONE',  ( 5.560781378645573980, 6.809993116116507654E-16, -4.000000000000000000 ) ) ;
#2393=( LENGTH_UNIT ( ) NAMED_UNIT ( * ) SI_UNIT ( .MILLI., .METRE. ) );
#2394=PRODUCT ( 'hex flange nut gradea_iso_ISO - 4161 - M5 - N', 'hex flange nut gradea_iso_ISO - 4161 - M5 - N', '', ( #8573 ) ) ;
#2397=CARTESIAN_POINT ( 'NONE',  ( 2.100000000000000089, 0.000000000000000000, -0.2800830152838844622 ) ) ;
#2434=DIRECTION ( 'NONE',  ( -0.000000000000000000, -0.000000000000000000, 1.000000000000000000 ) ) ;
#2440=VERTEX_POINT ( 'NONE', #6442 ) ;
#2446=VERTEX_POINT ( 'NONE', #4087 ) ;
#2462=CARTESIAN_POINT ( 'NONE',  ( -3.436319922987618902, 2.634841920961291439, -3.531542292955721862 ) ) ;
#2467=ORIENTED_EDGE ( 'NONE', *, *, #11904, .F. ) ;
#2469=LINE ( 'NONE', #155, #8755 ) ;
#2482=ORIENTED_EDGE ( 'NONE', *, *, #5036, .T. ) ;
#2488=EDGE_CURVE ( 'NONE', #4304, #4981, #12435, .T. ) ;
#2492=CARTESIAN_POINT ( 'NONE',  ( 3.453038570460273071, 2.625189405340834448, -3.535263753543585352 ) ) ;
#2502=DIRECTION ( 'NONE',  ( -1.000000000000000000, 0.000000000000000000, 0.000000000000000000 ) ) ;
#2508=ORIENTED_EDGE ( 'NONE', *, *, #7645, .T. ) ;
#2523=ADVANCED_FACE ( 'NONE', ( #7401 ), #11888, .T. ) ;
#2527=DIRECTION ( 'NONE',  ( -0.000000000000000000, 0.000000000000000000, -1.000000000000000000 ) ) ;
#2543=CARTESIAN_POINT ( 'NONE',  ( 0.000000000000000000, 0.000000000000000000, -4.000000000000000000 ) ) ;
#2547=AXIS2_PLACEMENT_3D ( 'NONE', #6636, #12304, #13206 ) ;
#2570=PLANE ( 'NONE',  #3114 ) ;
#2601=AXIS2_PLACEMENT_3D ( 'NONE', #1284, #3427, #10285 ) ;
#2609=EDGE_CURVE ( 'NONE', #3145, #2790, #3185, .T. ) ;
#2615=CARTESIAN_POINT ( 'NONE',  ( -1.149515148933662080E-15, -4.736529461166056443, -3.681130640444383317 ) ) ;
#2636=CARTESIAN_POINT ( 'NONE',  ( 0.6920835326022565237, 4.454600218803884459, -3.597382984111579862 ) ) ;
#2638=CARTESIAN_POINT ( 'NONE',  ( -3.453038570459499024, -2.625189405340453419, -3.535263753545272891 ) ) ;
#2646=DIRECTION ( 'NONE',  ( -1.000000000000000000, 0.000000000000000000, 0.000000000000000000 ) ) ;
#2648=CARTESIAN_POINT ( 'NONE',  ( 2.000000000000000444, 3.464101615137754830, -3.142992957459231018 ) ) ;
#2653=CARTESIAN_POINT ( 'NONE',  ( 0.5449313310647804220, 4.304185902836899835, -3.316620875263383894 ) ) ;
#2667=UNCERTAINTY_MEASURE_WITH_UNIT (LENGTH_MEASURE( 1.000000000000000082E-05 ), #14207, 'distance_accuracy_value', 'NONE');
#2680=DIRECTION ( 'NONE',  ( 0.000000000000000000, 0.000000000000000000, 1.000000000000000000 ) ) ;
#2695=CARTESIAN_POINT ( 'NONE',  ( -4.000000000000000000, 0.7924765000094600165, -0.05906175389889745803 ) ) ;
#2712=ORIENTED_EDGE ( 'NONE', *, *, #186, .F. ) ;
#2714=CARTESIAN_POINT ( 'NONE',  ( -2.682243648011671588, -3.070208061305317759, -0.04852650426602272971 ) ) ;
#2716=FACE_OUTER_BOUND ( 'NONE', #2939, .T. ) ;
#2755=CARTESIAN_POINT ( 'NONE',  ( 0.5469614295415388128, -4.303013824935362663, -3.535263753543555598 ) ) ;
#2758=CARTESIAN_POINT ( 'NONE',  ( -4.000000000000000000, 0.000000000000000000, 0.000000000000000000 ) ) ;
#2764=CARTESIAN_POINT ( 'NONE',  ( -4.000000000000000000, -2.309401076758515803, -0.4999999999999995559 ) ) ;
#2769=DIRECTION ( 'NONE',  ( -0.000000000000000000, 0.000000000000000000, -1.000000000000000000 ) ) ;
#2789=CARTESIAN_POINT ( 'NONE',  ( 3.540020015735602765, 2.810662092924382627, -3.602146406945867962 ) ) ;
#2790=VERTEX_POINT ( 'NONE', #4199 ) ;
#2799=ADVANCED_FACE ( 'NONE', ( #934 ), #2115, .T. ) ;
#2804=DIRECTION ( 'NONE',  ( 0.000000000000000000, 0.000000000000000000, -1.000000000000000000 ) ) ;
#2826=CARTESIAN_POINT ( 'NONE',  ( 4.000000000000000000, 0.7924765000094659007, -0.05906175389889852662 ) ) ;
#2835=CARTESIAN_POINT ( 'NONE',  ( 2.807080416178989513, -3.225969019225150003, -3.502507215260505014 ) ) ;
#2838=AXIS2_PLACEMENT_3D ( 'NONE', #9373, #9306, #2502 ) ;
#2848=CARTESIAN_POINT ( 'NONE',  ( 3.861362476283255685, 2.629030857715988656, -3.671615880910370500 ) ) ;
#2851=CARTESIAN_POINT ( 'NONE',  ( -2.756197834950067094, -3.027510591568735254, -3.223146290109809797 ) ) ;
#2904=CARTESIAN_POINT ( 'NONE',  ( 0.000000000000000000, 0.000000000000000000, -4.974599999999998801 ) ) ;
#2912=DIRECTION ( 'NONE',  ( 0.000000000000000000, -0.000000000000000000, 1.000000000000000000 ) ) ;
#2939=EDGE_LOOP ( 'NONE', ( #3305, #923 ) ) ;
#2955=CARTESIAN_POINT ( 'NONE',  ( -4.154094228333820915, -2.398367420967594921, -3.721909803043257803 ) ) ;
#2976=CARTESIAN_POINT ( 'NONE',  ( -2.100000000000000089, 2.571758278209441957E-16, -4.694516984716113228 ) ) ;
#2979=( NAMED_UNIT ( * ) PLANE_ANGLE_UNIT ( ) SI_UNIT ( $, .RADIAN. ) );
#2999=( BOUNDED_SURFACE ( )  B_SPLINE_SURFACE ( 3, 2, ( 
 ( #6258, #2236, #13386 ),
 ( #10756, #3282, #11026 ),
 ( #5158, #7651, #908 ),
 ( #6684, #11179, #5564 ),
 ( #4462, #2462, #10142 ),
 ( #4617, #9104, #4773 ) ),
 .UNSPECIFIED., .F., .F., .T. ) 
 B_SPLINE_SURFACE_WITH_KNOTS ( ( 4, 2, 4 ),
 ( 3, 3 ),
 ( 0.02032853247518125531, 0.02278863295364820865, 0.02524873343211516200 ),
 ( 0.000000000000000000, 1.000000000000000000 ),
 .UNSPECIFIED. ) 
 GEOMETRIC_REPRESENTATION_ITEM ( )  RATIONAL_B_SPLINE_SURFACE ( (
 ( 1.000000000000000000, 0.8047781615896836271, 1.000000000000000000),
 ( 1.000000000000000000, 0.8123767586289967202, 1.000000000000000000),
 ( 1.000000000000000000, 0.8190662415563443322, 1.000000000000000000),
 ( 1.000000000000000000, 0.8192361015669982205, 1.000000000000000000),
 ( 1.000000000000000000, 0.8126135807103181952, 1.000000000000000000),
 ( 1.000000000000000000, 0.8047712338318587788, 1.000000000000000000) ) ) 
 REPRESENTATION_ITEM ( '' )  SURFACE ( )  );
#3022=AXIS2_PLACEMENT_3D ( 'NONE', #9689, #8577, #9608 ) ;
#3048=EDGE_CURVE ( 'NONE', #6453, #3563, #7393, .T. ) ;
#3054=ORIENTED_EDGE ( 'NONE', *, *, #11417, .T. ) ;
#3059=EDGE_LOOP ( 'NONE', ( #11049, #12357, #12708, #11338 ) ) ;
#3061=ADVANCED_FACE ( 'NONE', ( #8316 ), #3991, .T. ) ;
#3068=EDGE_LOOP ( 'NONE', ( #13416, #5705, #5230, #9123 ) ) ;
#3069=CARTESIAN_POINT ( 'NONE',  ( 0.000000000000000000, 0.000000000000000000, 0.000000000000000000 ) ) ;
#3095=CIRCLE ( 'NONE', #1250, 4.000000000000000000 ) ;
#3110=( GEOMETRIC_REPRESENTATION_CONTEXT ( 3 ) GLOBAL_UNCERTAINTY_ASSIGNED_CONTEXT ( ( #12849 ) ) GLOBAL_UNIT_ASSIGNED_CONTEXT ( ( #12118, #2979, #7477 ) ) REPRESENTATION_CONTEXT ( 'NONE', 'WORKASPACE' ) );
#3114=AXIS2_PLACEMENT_3D ( 'NONE', #7220, #6119, #502 ) ;
#3118=CIRCLE ( 'NONE', #4532, 4.000000000000000000 ) ;
#3131=DIRECTION ( 'NONE',  ( -0.000000000000000000, -0.000000000000000000, 1.000000000000000000 ) ) ;
#3133=SURFACE_SIDE_STYLE ('',( #6377 ) ) ;
#3145=VERTEX_POINT ( 'NONE', #4049 ) ;
#3147=FACE_OUTER_BOUND ( 'NONE', #13031, .T. ) ;
#3168=ORIENTED_EDGE ( 'NONE', *, *, #10986, .T. ) ;
#3184=EDGE_LOOP ( 'NONE', ( #12737, #4793, #11521 ) ) ;
#3185=B_SPLINE_CURVE_WITH_KNOTS ( 'NONE', 3,
 ( #278, #11504, #4593, #13877, #13654, #8049 ),
 .UNSPECIFIED., .F., .F.,
 ( 4, 2, 4 ),
 ( 4.336808689942017736E-19, 0.0002095117440864781224, 0.0004190234881729558111 ),
 .UNSPECIFIED. ) ;
#3196=DIRECTION ( 'NONE',  ( 0.000000000000000000, 0.000000000000000000, 1.000000000000000000 ) ) ;
#3205=CARTESIAN_POINT ( 'NONE',  ( -5.560781378645575757, 6.809993116116508640E-16, -4.000000000000000000 ) ) ;
#3219=DIRECTION ( 'NONE',  ( 0.000000000000000000, -0.000000000000000000, 1.000000000000000000 ) ) ;
#3255=LINE ( 'NONE', #2364, #12230 ) ;
#3282=CARTESIAN_POINT ( 'NONE',  ( -0.5469614295416921346, 4.303013824936271270, -3.535263753543735454 ) ) ;
#3295=CARTESIAN_POINT ( 'NONE',  ( 0.000000000000000000, 0.000000000000000000, -5.000000000000000888 ) ) ;
#3305=ORIENTED_EDGE ( 'NONE', *, *, #7056, .F. ) ;
#3306=ADVANCED_FACE ( 'NONE', ( #4382 ), #8877, .F. ) ;
#3353=ORIENTED_EDGE ( 'NONE', *, *, #5219, .F. ) ;
#3355=CARTESIAN_POINT ( 'NONE',  ( -1.747541505913277282, 3.837784562140256650, -3.503702292528906526 ) ) ;
#3363=CARTESIAN_POINT ( 'NONE',  ( 0.6448876103708359731, 4.246476118072354922, -0.2256878752776725616 ) ) ;
#3373=DIRECTION ( 'NONE',  ( 0.000000000000000000, 0.000000000000000000, 1.000000000000000000 ) ) ;
#3377=EDGE_CURVE ( 'NONE', #1238, #1371, #4765, .T. ) ;
#3394=CARTESIAN_POINT ( 'NONE',  ( 4.211140560182196957, -2.431303136016555122, -3.745885042887436622 ) ) ;
#3415=PLANE ( 'NONE',  #5389 ) ;
#3419=VERTEX_POINT ( 'NONE', #11733 ) ;
#3420=CARTESIAN_POINT ( 'NONE',  ( -0.6937372685066653943, 4.453844082567723461, -3.610536846335889116 ) ) ;
#3427=DIRECTION ( 'NONE',  ( 0.000000000000000000, 0.000000000000000000, -1.000000000000000000 ) ) ;
#3454=CARTESIAN_POINT ( 'NONE',  ( 4.000000000000000000, 0.000000000000000000, 0.000000000000000000 ) ) ;
#3457=LINE ( 'NONE', #6855, #7359 ) ;
#3460=EDGE_CURVE ( 'NONE', #11959, #4981, #9610, .T. ) ;
#3467=B_SPLINE_CURVE_WITH_KNOTS ( 'NONE', 3,
 ( #4824, #6949, #3925, #1491, #9245, #10423, #5989, #12780 ),
 .UNSPECIFIED., .F., .F.,
 ( 4, 2, 2, 4 ),
 ( 2.465131517390770070E-07, 0.001183067374689869946, 0.001774477805458935659, 0.002365888236228001588 ),
 .UNSPECIFIED. ) ;
#3475=CIRCLE ( 'NONE', #14545, 5.560781378645573980 ) ;
#3498=CARTESIAN_POINT ( 'NONE',  ( 1.734723475976807094E-15, 4.618802153517012954, -0.4999999999999995559 ) ) ;
#3521=CARTESIAN_POINT ( 'NONE',  ( 2.500000000000000888, 3.061616997868384127E-16, -4.974599999999998801 ) ) ;
#3525=ORIENTED_EDGE ( 'NONE', *, *, #13842, .F. ) ;
#3526=CIRCLE ( 'NONE', #3988, 4.000000000000000000 ) ;
#3538=CIRCLE ( 'NONE', #1646, 4.000000000000000000 ) ;
#3550=ORIENTED_EDGE ( 'NONE', *, *, #10986, .F. ) ;
#3563=VERTEX_POINT ( 'NONE', #9977 ) ;
#3580=ORIENTED_EDGE ( 'NONE', *, *, #9510, .T. ) ;
#3599=CONICAL_SURFACE ( 'NONE', #11825, 4.000000000000000000, 0.8911886515913786111 ) ;
#3606=EDGE_CURVE ( 'NONE', #2314, #10556, #3255, .T. ) ;
#3607=DIRECTION ( 'NONE',  ( -0.000000000000000000, -0.000000000000000000, 1.000000000000000000 ) ) ;
#3629=CARTESIAN_POINT ( 'NONE',  ( 4.211140560182196957, 2.431303136016536470, -3.745885042887433514 ) ) ;
#3634=B_SPLINE_CURVE_WITH_KNOTS ( 'NONE', 3,
 ( #6414, #9737, #924, #5447, #7436, #14455, #4125, #8615 ),
 .UNSPECIFIED., .F., .F.,
 ( 4, 2, 2, 4 ),
 ( 2.465131517071610173E-07, 0.001183067374689837636, 0.001774477805458902699, 0.002365888236227967761 ),
 .UNSPECIFIED. ) ;
#3673=ORIENTED_EDGE ( 'NONE', *, *, #13691, .F. ) ;
#3681=CARTESIAN_POINT ( 'NONE',  ( -4.000000000000000000, -0.3979232138631226823, -3.896351557369779711E-17 ) ) ;
#3688=DIRECTION ( 'NONE',  ( -1.000000000000000000, 0.000000000000000000, 0.000000000000000000 ) ) ;
#3691=FACE_OUTER_BOUND ( 'NONE', #5407, .T. ) ;
#3707=EDGE_CURVE ( 'NONE', #3419, #14577, #12692, .T. ) ;
#3723=CARTESIAN_POINT ( 'NONE',  ( -6.259644161404860030E-16, -4.618802153517027165, -3.433295621305388234 ) ) ;
#3739=CYLINDRICAL_SURFACE ( 'NONE', #13848, 2.100000000000000089 ) ;
#3767=CARTESIAN_POINT ( 'NONE',  ( -4.000000000000000000, 2.471528634177585282, -3.686887442155186712 ) ) ;
#3799=CARTESIAN_POINT ( 'NONE',  ( -2.500000000000000888, 0.000000000000000000, -4.974599999999998801 ) ) ;
#3815=VERTEX_POINT ( 'NONE', #5764 ) ;
#3846=CARTESIAN_POINT ( 'NONE',  ( -3.999999999998910649, -1.658469974638591804, -3.531532913075256186 ) ) ;
#3851=VERTEX_POINT ( 'NONE', #9673 ) ;
#3854=CARTESIAN_POINT ( 'NONE',  ( 2.344047193898588954, 3.265465875126468021, -5.031375706690542042E-16 ) ) ;
#3855=CARTESIAN_POINT ( 'NONE',  ( -2.000000000000006661, 3.464101615137750834, 0.000000000000000000 ) ) ;
#3869=CARTESIAN_POINT ( 'NONE',  ( 4.000000000000000000, 2.309401076758497151, -3.433295621305379353 ) ) ;
#3885=CARTESIAN_POINT ( 'NONE',  ( 3.522875095019493141, -2.820352903225631369, -3.598441714920572299 ) ) ;
#3925=CARTESIAN_POINT ( 'NONE',  ( -0.6448876103708541807, -4.246476118072358474, -0.2256878752776773356 ) ) ;
#3931=CARTESIAN_POINT ( 'NONE',  ( -4.000000000000000000, 2.309401076758498483, -5.000000000000000000 ) ) ;
#3944=CARTESIAN_POINT ( 'NONE',  ( -4.211140560182196957, 2.431303136016537803, -3.745885042887433514 ) ) ;
#3946=ORIENTED_EDGE ( 'NONE', *, *, #12408, .T. ) ;
#3958=DIRECTION ( 'NONE',  ( -0.000000000000000000, -0.000000000000000000, 1.000000000000000000 ) ) ;
#3988=AXIS2_PLACEMENT_3D ( 'NONE', #10730, #3131, #756 ) ;
#3991=CONICAL_SURFACE ( 'NONE', #6108, 4.000000000000000000, 0.8911886515913786111 ) ;
#4049=CARTESIAN_POINT ( 'NONE',  ( 4.000000000000000000, -2.309401076758514915, -3.433295621305383349 ) ) ;
#4063=ORIENTED_EDGE ( 'NONE', *, *, #12359, .T. ) ;
#4065=ORIENTED_EDGE ( 'NONE', *, *, #8983, .T. ) ;
#4083=CIRCLE ( 'NONE', #13988, 0.5155456020628804703 ) ;
#4087=CARTESIAN_POINT ( 'NONE',  ( -6.259644161404860030E-16, -4.618802153517027165, -3.433295621305388234 ) ) ;
#4102=CARTESIAN_POINT ( 'NONE',  ( 2.691179338796023329E-15, 4.647089433458991614, -3.572167766733753691 ) ) ;
#4117=VERTEX_POINT ( 'NONE', #4801 ) ;
#4125=CARTESIAN_POINT ( 'NONE',  ( 2.171643655288379993, -3.365003104552334978, -1.195831703456429434E-14 ) ) ;
#4130=EDGE_CURVE ( 'NONE', #2290, #10969, #1253, .T. ) ;
#4150=ORIENTED_EDGE ( 'NONE', *, *, #5627, .T. ) ;
#4152=DIRECTION ( 'NONE',  ( -0.5000000000000019984, -0.8660254037844375974, 0.000000000000000000 ) ) ;
#4158=CARTESIAN_POINT ( 'NONE',  ( 5.384454397937118664, 0.000000000000000000, -4.484454397937119197 ) ) ;
#4161=CARTESIAN_POINT ( 'NONE',  ( -3.974357786152442180E-13, 4.796734841935204052, -3.721909803043259579 ) ) ;
#4199=CARTESIAN_POINT ( 'NONE',  ( 4.211140560182196957, -2.431303136016555122, -3.745885042887436622 ) ) ;
#4206=CARTESIAN_POINT ( 'NONE',  ( -3.999999999999999112, -2.309401076758512694, -3.504269196027871125 ) ) ;
#4220=EDGE_LOOP ( 'NONE', ( #1177, #14051, #6741, #4063, #7686, #11712, #2508 ) ) ;
#4240=ORIENTED_EDGE ( 'NONE', *, *, #8287, .T. ) ;
#4245=AXIS2_PLACEMENT_3D ( 'NONE', #6695, #7586, #784 ) ;
#4248=ORIENTED_EDGE ( 'NONE', *, *, #13992, .T. ) ;
#4285=CARTESIAN_POINT ( 'NONE',  ( -6.473970235329672780E-16, -4.862606272033106691, -3.745885042887442395 ) ) ;
#4304=VERTEX_POINT ( 'NONE', #10688 ) ;
#4320=CARTESIAN_POINT ( 'NONE',  ( -4.211140560182196957, 2.431303136016537803, -3.745885042887433514 ) ) ;
#4326=EDGE_LOOP ( 'NONE', ( #3946, #4240, #10995, #8931 ) ) ;
#4336=B_SPLINE_CURVE_WITH_KNOTS ( 'NONE', 3,
 ( #4975, #9475, #13979, #13674, #3869 ),
 .UNSPECIFIED., .F., .F.,
 ( 4, 1, 4 ),
 ( 0.000000000000000000, 0.002309401076758505790, 0.004618802153517011580 ),
 .UNSPECIFIED. ) ;
#4347=CARTESIAN_POINT ( 'NONE',  ( 0.000000000000000000, 0.000000000000000000, 0.000000000000000000 ) ) ;
#4381=CARTESIAN_POINT ( 'NONE',  ( -1.999999999999999556, 3.464101615137754830, -3.142992957459232795 ) ) ;
#4382=FACE_OUTER_BOUND ( 'NONE', #14060, .T. ) ;
#4385=EDGE_CURVE ( 'NONE', #8837, #1371, #1069, .T. ) ;
#4397=EDGE_CURVE ( 'NONE', #8837, #7674, #8721, .T. ) ;
#4404=DIRECTION ( 'NONE',  ( -1.000000000000000000, 0.000000000000000000, 0.000000000000000000 ) ) ;
#4408=ADVANCED_FACE ( 'NONE', ( #5516 ), #8484, .F. ) ;
#4418=CARTESIAN_POINT ( 'NONE',  ( 1.747541505913279281, -3.837784562140273081, -3.503702292528912299 ) ) ;
#4462=CARTESIAN_POINT ( 'NONE',  ( -3.455068668934486276, 2.624017327439035707, -3.316620875263955437 ) ) ;
#4470=ORIENTED_EDGE ( 'NONE', *, *, #6275, .T. ) ;
#4471=CARTESIAN_POINT ( 'NONE',  ( -2.500000000000000444, 3.061616997868383634E-16, -5.000000000000000888 ) ) ;
#4489=AXIS2_PLACEMENT_3D ( 'NONE', #13991, #2527, #6157 ) ;
#4502=CONICAL_SURFACE ( 'NONE', #13920, 5.560781378645573980, 1.221730476396046816 ) ;
#4514=AXIS2_PLACEMENT_3D ( 'NONE', #710, #11779, #5303 ) ;
#4528=ADVANCED_FACE ( 'NONE', ( #6544 ), #7067, .T. ) ;
#4532=AXIS2_PLACEMENT_3D ( 'NONE', #9850, #9784, #8670 ) ;
#4536=ORIENTED_EDGE ( 'NONE', *, *, #1667, .T. ) ;
#4550=EDGE_LOOP ( 'NONE', ( #11695, #10277, #4470, #11035 ) ) ;
#4566=LINE ( 'NONE', #3521, #4946 ) ;
#4567=CARTESIAN_POINT ( 'NONE',  ( -4.197393957002303999, -0.8151795401431414234, -3.503767560748935139 ) ) ;
#4593=CARTESIAN_POINT ( 'NONE',  ( 4.024499207728847949, -2.323545700935699454, -3.572172305156873673 ) ) ;
#4603=( BOUNDED_SURFACE ( )  B_SPLINE_SURFACE ( 3, 2, ( 
 ( #8248, #11708, #4944 ),
 ( #11573, #2492, #2789 ),
 ( #5026, #6993, #14022 ),
 ( #568, #10694, #9295 ),
 ( #2653, #1537, #10621 ),
 ( #12761, #1692, #13798 ) ),
 .UNSPECIFIED., .F., .F., .T. ) 
 B_SPLINE_SURFACE_WITH_KNOTS ( ( 4, 2, 4 ),
 ( 3, 3 ),
 ( 0.02032853247518126225, 0.02278863295364821212, 0.02524873343211516200 ),
 ( 0.000000000000000000, 1.000000000000000000 ),
 .UNSPECIFIED. ) 
 GEOMETRIC_REPRESENTATION_ITEM ( )  RATIONAL_B_SPLINE_SURFACE ( (
 ( 1.000000000000000000, 0.8047781615896835161, 1.000000000000000000),
 ( 1.000000000000000000, 0.8123767586291043008, 1.000000000000000000),
 ( 1.000000000000000000, 0.8190662415562011134, 1.000000000000000000),
 ( 1.000000000000000000, 0.8192361015671398849, 1.000000000000000000),
 ( 1.000000000000000000, 0.8126135807102121689, 1.000000000000000000),
 ( 1.000000000000000000, 0.8047712338318585568, 1.000000000000000000) ) ) 
 REPRESENTATION_ITEM ( '' )  SURFACE ( )  );
#4610=CARTESIAN_POINT ( 'NONE',  ( -2.805705207896067144, 3.226868319750155312, -3.503898532754364581 ) ) ;
#4617=CARTESIAN_POINT ( 'NONE',  ( -4.175648173966055587, 2.207990556236529844, -3.469390959564062626 ) ) ;
#4632=LINE ( 'NONE', #8016, #7473 ) ;
#4659=B_SPLINE_CURVE_WITH_KNOTS ( 'NONE', 3,
 ( #13072, #2955, #11937, #8263, #4206, #5529 ),
 .UNSPECIFIED., .F., .F.,
 ( 4, 2, 4 ),
 ( -3.640115492409406142E-06, 0.0002066546034003385283, 0.0004169493222930864334 ),
 .UNSPECIFIED. ) ;
#4670=B_SPLINE_CURVE_WITH_KNOTS ( 'NONE', 3,
 ( #11195, #9282, #13557, #170, #4711, #2326 ),
 .UNSPECIFIED., .F., .F.,
 ( 4, 2, 4 ),
 ( 0.002365888236227967761, 0.003551327329835077609, 0.004736766423442186590 ),
 .UNSPECIFIED. ) ;
#4672=FACE_OUTER_BOUND ( 'NONE', #2209, .T. ) ;
#4681=EDGE_CURVE ( 'NONE', #1630, #11949, #4999, .T. ) ;
#4682=CARTESIAN_POINT ( 'NONE',  ( 4.000000000000000888, 0.8228435280416209752, -3.430609588141487976 ) ) ;
#4711=CARTESIAN_POINT ( 'NONE',  ( 0.3208286057739604957, -4.433571671609698228, -0.3503314178412692548 ) ) ;
#4731=FACE_OUTER_BOUND ( 'NONE', #4220, .T. ) ;
#4741=ORIENTED_EDGE ( 'NONE', *, *, #11904, .T. ) ;
#4765=LINE ( 'NONE', #3799, #7763 ) ;
#4769=EDGE_LOOP ( 'NONE', ( #11308, #11042, #7080, #978, #5555 ) ) ;
#4773=CARTESIAN_POINT ( 'NONE',  ( -4.236525694536558362, 2.416953475386465211, -3.751298745799836354 ) ) ;
#4790=CARTESIAN_POINT ( 'NONE',  ( -1.274258131565027874, -3.883108878240886241, -3.220599429844051009 ) ) ;
#4793=ORIENTED_EDGE ( 'NONE', *, *, #14141, .T. ) ;
#4801=CARTESIAN_POINT ( 'NONE',  ( -4.211140560182196957, 2.431303136016537803, -3.745885042887433514 ) ) ;
#4824=CARTESIAN_POINT ( 'NONE',  ( -2.688821387764050996E-14, -4.618802153517012954, -0.4999999999999995559 ) ) ;
#4842=ORIENTED_EDGE ( 'NONE', *, *, #11654, .T. ) ;
#4843=CARTESIAN_POINT ( 'NONE',  ( 1.257172072275274388, -3.892973519170983110, -3.433252694550781303 ) ) ;
#4851=CARTESIAN_POINT ( 'NONE',  ( 4.197393957002303999, 7.772902908466098641E-14, -3.503767560748929810 ) ) ;
#4854=CARTESIAN_POINT ( 'NONE',  ( 4.211140560182196957, 2.431303136016536470, -3.745885042887433514 ) ) ;
#4872=DIRECTION ( 'NONE',  ( -0.000000000000000000, -0.000000000000000000, 1.000000000000000000 ) ) ;
#4911=ORIENTED_EDGE ( 'NONE', *, *, #4130, .T. ) ;
#4931=VERTEX_POINT ( 'NONE', #2162 ) ;
#4944=CARTESIAN_POINT ( 'NONE',  ( 4.235886605889389145, 2.417314728048528760, -3.751161874094018245 ) ) ;
#4946=VECTOR ( 'NONE', #2105, 1000.000000000000114 ) ;
#4975=CARTESIAN_POINT ( 'NONE',  ( 4.000000000000000000, -2.309401076758514915, -3.433295621305383349 ) ) ;
#4981=VERTEX_POINT ( 'NONE', #3205 ) ;
#4982=EDGE_CURVE ( 'NONE', #2440, #5056, #578, .T. ) ;
#4986=ADVANCED_FACE ( 'NONE', ( #900 ), #7619, .F. ) ;
#4999=LINE ( 'NONE', #14217, #12731 ) ;
#5002=B_SPLINE_CURVE_WITH_KNOTS ( 'NONE', 3,
 ( #3394, #11275, #5527, #4418, #8918, #9067, #13565, #4285 ),
 .UNSPECIFIED., .F., .F.,
 ( 4, 2, 2, 4 ),
 ( 0.000000000000000000, 0.002450665683189819262, 0.003675998524784728893, 0.004901331366379639391 ),
 .UNSPECIFIED. ) ;
#5006=CARTESIAN_POINT ( 'NONE',  ( 2.449848172108560096, 3.432307619358740514, -3.503702292528905637 ) ) ;
#5008=CARTESIAN_POINT ( 'NONE',  ( -4.140404888673278272, -2.228338276487456415, -3.686887068327035166 ) ) ;
#5014=EDGE_LOOP ( 'NONE', ( #8276, #11969, #5300, #9186 ) ) ;
#5016=CARTESIAN_POINT ( 'NONE',  ( 4.024499207728848837, 2.323545700935681246, -3.572172305156870564 ) ) ;
#5026=CARTESIAN_POINT ( 'NONE',  ( 2.756197834950227410, 3.027510591568626896, -3.223146290109805356 ) ) ;
#5036=EDGE_CURVE ( 'NONE', #11959, #4117, #5867, .T. ) ;
#5056=VERTEX_POINT ( 'NONE', #3855 ) ;
#5077=FACE_OUTER_BOUND ( 'NONE', #4550, .T. ) ;
#5093=CARTESIAN_POINT ( 'NONE',  ( -4.000000000000000000, -1.680117682357936904, -3.316611593218794951 ) ) ;
#5122=CARTESIAN_POINT ( 'NONE',  ( 2.100000000000000089, 0.000000000000000000, -4.694516984716113228 ) ) ;
#5126=CARTESIAN_POINT ( 'NONE',  ( -4.101948962586059011, 2.368261337751163875, -3.681124513963739187 ) ) ;
#5129=CARTESIAN_POINT ( 'NONE',  ( -4.000000000000000000, 0.9868501483902560878, -0.09357334158579519445 ) ) ;
#5138=FACE_OUTER_BOUND ( 'NONE', #1806, .T. ) ;
#5156=CARTESIAN_POINT ( 'NONE',  ( -2.344047193898593395, -3.265465875126480455, -1.054683074273691752E-14 ) ) ;
#5158=CARTESIAN_POINT ( 'NONE',  ( -1.243802165048909503, 3.900692638707381921, -3.223146290109805800 ) ) ;
#5161=CARTESIAN_POINT ( 'NONE',  ( -4.000000000000000000, -2.472261339043343220, -3.687027428081192326 ) ) ;
#5200=CARTESIAN_POINT ( 'NONE',  ( -3.333333333333332149, -2.694301256218264218, -3.300726591567082036 ) ) ;
#5217=CARTESIAN_POINT ( 'NONE',  ( 0.000000000000000000, 0.000000000000000000, -4.974599999999998801 ) ) ;
#5219=EDGE_CURVE ( 'NONE', #992, #10412, #9038, .T. ) ;
#5220=CARTESIAN_POINT ( 'NONE',  ( 0.000000000000000000, 0.000000000000000000, -0.3080913168122742518 ) ) ;
#5229=ORIENTED_EDGE ( 'NONE', *, *, #5384, .T. ) ;
#5230=ORIENTED_EDGE ( 'NONE', *, *, #6916, .F. ) ;
#5277=SHAPE_REPRESENTATION_RELATIONSHIP ( 'NONE' , 'NONE' ,  #6779, #7024 ) ;
#5278=EDGE_CURVE ( 'NONE', #2790, #1880, #5002, .T. ) ;
#5289=DIRECTION ( 'NONE',  ( -1.000000000000000000, 0.000000000000000000, 0.000000000000000000 ) ) ;
#5294=ORIENTED_EDGE ( 'NONE', *, *, #5863, .T. ) ;
#5300=ORIENTED_EDGE ( 'NONE', *, *, #7197, .T. ) ;
#5303=DIRECTION ( 'NONE',  ( 1.000000000000000000, 0.000000000000000000, 0.000000000000000000 ) ) ;
#5336=B_SPLINE_CURVE_WITH_KNOTS ( 'NONE', 3,
 ( #3498, #987, #3363, #1207, #9999, #2235, #5716, #8823 ),
 .UNSPECIFIED., .F., .F.,
 ( 4, 2, 2, 4 ),
 ( 2.465131517075058656E-07, 0.001183067374689851080, 0.001774477805458923299, 0.002365888236227995517 ),
 .UNSPECIFIED. ) ;
#5339=CARTESIAN_POINT ( 'NONE',  ( 0.000000000000000000, 0.000000000000000000, -0.2800830152838844622 ) ) ;
#5351=DIRECTION ( 'NONE',  ( -1.000000000000000000, 0.000000000000000000, 0.000000000000000000 ) ) ;
#5355=EDGE_LOOP ( 'NONE', ( #10376, #6720 ) ) ;
#5372=EDGE_LOOP ( 'NONE', ( #2331, #11282, #2467 ) ) ;
#5384=EDGE_CURVE ( 'NONE', #6453, #1630, #1634, .T. ) ;
#5389=AXIS2_PLACEMENT_3D ( 'NONE', #5701, #5836, #10340 ) ;
#5400=CIRCLE ( 'NONE', #9163, 5.384454397937118664 ) ;
#5402=AXIS2_PLACEMENT_3D ( 'NONE', #14562, #13379, #11169 ) ;
#5407=EDGE_LOOP ( 'NONE', ( #422, #9481, #2036, #5942 ) ) ;
#5420=CARTESIAN_POINT ( 'NONE',  ( -3.333333333333335258, 2.694301256218251783, -3.300726591567079815 ) ) ;
#5428=ORIENTED_EDGE ( 'NONE', *, *, #9139, .T. ) ;
#5447=CARTESIAN_POINT ( 'NONE',  ( 2.855764796983346177, -2.970025579236428737, -0.09382832055446485575 ) ) ;
#5467=CARTESIAN_POINT ( 'NONE',  ( 4.000000000000000000, 0.000000000000000000, 0.000000000000000000 ) ) ;
#5478=CARTESIAN_POINT ( 'NONE',  ( -2.688821387764050996E-14, -4.618802153517012954, -0.4999999999999995559 ) ) ;
#5479=ADVANCED_FACE ( 'NONE', ( #12897 ), #10874, .T. ) ;
#5516=FACE_OUTER_BOUND ( 'NONE', #5014, .T. ) ;
#5527=CARTESIAN_POINT ( 'NONE',  ( 2.805705207896068476, -3.226868319750173075, -3.503898532754370354 ) ) ;
#5529=CARTESIAN_POINT ( 'NONE',  ( -4.000000000000000000, -2.309401076758512694, -3.433295621305382461 ) ) ;
#5555=ORIENTED_EDGE ( 'NONE', *, *, #6621, .T. ) ;
#5564=CARTESIAN_POINT ( 'NONE',  ( -2.807080416178626692, 3.225969019225154444, -3.502507215260441065 ) ) ;
#5565=CARTESIAN_POINT ( 'NONE',  ( -0.6507732100473471171, 4.243078065514775510, -0.2236248678334823436 ) ) ;
#5627=EDGE_CURVE ( 'NONE', #1238, #6877, #1200, .T. ) ;
#5631=CARTESIAN_POINT ( 'NONE',  ( 4.000000000000000000, 1.680228229147133767, -3.316631783032546021 ) ) ;
#5662=CARTESIAN_POINT ( 'NONE',  ( -4.197393957002303999, -7.773935952363655451E-14, -3.503767560748929810 ) ) ;
#5666=DIRECTION ( 'NONE',  ( 1.000000000000000000, 0.000000000000000000, 0.000000000000000000 ) ) ;
#5701=CARTESIAN_POINT ( 'NONE',  ( -6.259644161404860030E-16, -4.618802153517027165, -5.000000000000000000 ) ) ;
#5705=ORIENTED_EDGE ( 'NONE', *, *, #9090, .F. ) ;
#5716=CARTESIAN_POINT ( 'NONE',  ( 1.828356344711641102, 3.563200125723180900, -5.433716356636336675E-16 ) ) ;
#5764=CARTESIAN_POINT ( 'NONE',  ( 5.384454397937118664, 0.000000000000000000, -5.000000000000000000 ) ) ;
#5772=LINE ( 'NONE', #6672, #12486 ) ;
#5778=CARTESIAN_POINT ( 'NONE',  ( 4.000000000000000000, 0.8378280264232961239, -3.220590601395640018 ) ) ;
#5807=PRODUCT_DEFINITION_SHAPE ( 'NONE', 'NONE',  #10810 ) ;
#5819=ORIENTED_EDGE ( 'NONE', *, *, #5627, .F. ) ;
#5836=DIRECTION ( 'NONE',  ( 0.5000000000000013323, -0.8660254037844379305, 0.000000000000000000 ) ) ;
#5863=EDGE_CURVE ( 'NONE', #10556, #4981, #3475, .T. ) ;
#5867=B_SPLINE_CURVE_WITH_KNOTS ( 'NONE', 3,
 ( #13537, #71, #1202, #7986, #6958, #11653 ),
 .UNSPECIFIED., .F., .F.,
 ( 4, 2, 4 ),
 ( 0.002452478801916376308, 0.003676905084148007850, 0.004901331366379639391 ),
 .UNSPECIFIED. ) ;
#5935=CONICAL_SURFACE ( 'NONE', #6880, 4.000000000000000000, 0.8911886515913786111 ) ;
#5942=ORIENTED_EDGE ( 'NONE', *, *, #13987, .F. ) ;
#5980=ORIENTED_EDGE ( 'NONE', *, *, #11528, .T. ) ;
#5982=CARTESIAN_POINT ( 'NONE',  ( 3.679171394226031122, 2.494631558665830973, -0.3503314178412474389 ) ) ;
#5985=CARTESIAN_POINT ( 'NONE',  ( 0.000000000000000000, 0.000000000000000000, 0.000000000000000000 ) ) ;
#5987=ORIENTED_EDGE ( 'NONE', *, *, #5384, .F. ) ;
#5989=CARTESIAN_POINT ( 'NONE',  ( -1.828356344711647319, -3.563200125723192002, -1.076197711133951296E-14 ) ) ;
#6021=CARTESIAN_POINT ( 'NONE',  ( -1.390230914382372118, -4.043987460488664532, -3.502507215260523665 ) ) ;
#6029=CARTESIAN_POINT ( 'NONE',  ( -4.000000000000000000, -2.309401076758515803, -0.4999999999999995559 ) ) ;
#6033=CARTESIAN_POINT ( 'NONE',  ( -4.000000000000000000, -2.309401076758515803, -0.4999999999999995559 ) ) ;
#6037=CARTESIAN_POINT ( 'NONE',  ( -4.000000000000000000, 1.700094919196744270, -3.320312364301766017 ) ) ;
#6047=CARTESIAN_POINT ( 'NONE',  ( 3.999999999999998224, 2.472263674411418588, -3.687027874309861897 ) ) ;
#6057=B_SPLINE_CURVE_WITH_KNOTS ( 'NONE', 3,
 ( #6384, #14494, #4381, #5420, #8875 ),
 .UNSPECIFIED., .F., .F.,
 ( 4, 1, 4 ),
 ( 0.000000000000000000, 0.002309401076758506657, 0.004618802153517013315 ),
 .UNSPECIFIED. ) ;
#6069=B_SPLINE_CURVE_WITH_KNOTS ( 'NONE', 3,
 ( #14085, #5156, #2714, #8468, #11923, #6033 ),
 .UNSPECIFIED., .F., .F.,
 ( 4, 2, 4 ),
 ( 0.002365888236228001588, 0.003551327329835089319, 0.004736766423442177049 ),
 .UNSPECIFIED. ) ;
#6072=CIRCLE ( 'NONE', #7484, 2.100000000000000089 ) ;
#6089=B_SPLINE_CURVE_WITH_KNOTS ( 'NONE', 3,
 ( #9622, #4161, #12116, #4102, #14123, #13094 ),
 .UNSPECIFIED., .F., .F.,
 ( 4, 2, 4 ),
 ( -3.640115492407174633E-06, 0.0002066546034003413743, 0.0004169493222930899571 ),
 .UNSPECIFIED. ) ;
#6108=AXIS2_PLACEMENT_3D ( 'NONE', #9579, #6526, #2646 ) ;
#6119=DIRECTION ( 'NONE',  ( 0.000000000000000000, 0.000000000000000000, -1.000000000000000000 ) ) ;
#6128=EDGE_CURVE ( 'NONE', #3145, #6453, #4336, .T. ) ;
#6136=AXIS2_PLACEMENT_3D ( 'NONE', #2904, #8578, #9976 ) ;
#6149=CONICAL_SURFACE ( 'NONE', #8751, 4.000000000000000000, 0.8911886515913786111 ) ;
#6150=VECTOR ( 'NONE', #13434, 999.9999999999998863 ) ;
#6157=DIRECTION ( 'NONE',  ( -1.000000000000000000, 0.000000000000000000, 0.000000000000000000 ) ) ;
#6161=CARTESIAN_POINT ( 'NONE',  ( -6.473970235329672780E-16, -4.862606272033106691, -3.745885042887442395 ) ) ;
#6175=FACE_OUTER_BOUND ( 'NONE', #6679, .T. ) ;
#6199=FACE_OUTER_BOUND ( 'NONE', #6508, .T. ) ;
#6202=EDGE_CURVE ( 'NONE', #6883, #11959, #8747, .T. ) ;
#6210=ORIENTED_EDGE ( 'NONE', *, *, #10243, .T. ) ;
#6219=EDGE_LOOP ( 'NONE', ( #9754, #3525, #13052, #5, #13074, #14244 ) ) ;
#6231=ORIENTED_EDGE ( 'NONE', *, *, #9158, .F. ) ;
#6244=FACE_OUTER_BOUND ( 'NONE', #8366, .T. ) ;
#6258=CARTESIAN_POINT ( 'NONE',  ( 0.1750025118121568690, 4.719839900820621104, -3.469254087858248070 ) ) ;
#6275=EDGE_CURVE ( 'NONE', #7674, #10838, #4632, .T. ) ;
#6285=DIRECTION ( 'NONE',  ( -0.000000000000000000, -0.000000000000000000, 1.000000000000000000 ) ) ;
#6291=FACE_OUTER_BOUND ( 'NONE', #6219, .T. ) ;
#6294=FILL_AREA_STYLE_COLOUR ( '', #12532 ) ;
#6297=CARTESIAN_POINT ( 'NONE',  ( -6.259644161404860030E-16, -4.618802153517027165, -3.433295621305388234 ) ) ;
#6349=PRODUCT_DEFINITION_CONTEXT ( 'detailed design', #1983, 'design' ) ;
#6365=EDGE_CURVE ( 'NONE', #6877, #1238, #6072, .T. ) ;
#6377=SURFACE_STYLE_FILL_AREA ( #9915 ) ;
#6379=ADVANCED_FACE ( 'NONE', ( #6244 ), #9033, .F. ) ;
#6384=CARTESIAN_POINT ( 'NONE',  ( 1.567478505476134606E-15, 4.618802153517012066, -3.433295621305382905 ) ) ;
#6399=EDGE_CURVE ( 'NONE', #8478, #6458, #10550, .T. ) ;
#6414=CARTESIAN_POINT ( 'NONE',  ( 4.000000000000000000, -2.309401076758516691, -0.4999999999999995559 ) ) ;
#6417=DIRECTION ( 'NONE',  ( 1.000000000000000000, 0.000000000000000000, 0.000000000000000000 ) ) ;
#6442=CARTESIAN_POINT ( 'NONE',  ( -4.000000000000000000, 2.309401076758498483, -0.4999999999999927280 ) ) ;
#6450=ORIENTED_EDGE ( 'NONE', *, *, #4681, .T. ) ;
#6453=VERTEX_POINT ( 'NONE', #14360 ) ;
#6458=VERTEX_POINT ( 'NONE', #2090 ) ;
#6473=EDGE_LOOP ( 'NONE', ( #11598, #3054, #2026 ) ) ;
#6486=DIRECTION ( 'NONE',  ( -0.000000000000000000, -0.000000000000000000, 1.000000000000000000 ) ) ;
#6487=ADVANCED_FACE ( 'NONE', ( #7712 ), #13618, .F. ) ;
#6508=EDGE_LOOP ( 'NONE', ( #14266, #13697, #10010, #332, #1417 ) ) ;
#6516=DIRECTION ( 'NONE',  ( 0.000000000000000000, 0.000000000000000000, -1.000000000000000000 ) ) ;
#6526=DIRECTION ( 'NONE',  ( 0.000000000000000000, 0.000000000000000000, -1.000000000000000000 ) ) ;
#6527=CARTESIAN_POINT ( 'NONE',  ( -2.171643655288372443, 3.365003104552320767, 2.541098841762897165E-18 ) ) ;
#6544=FACE_OUTER_BOUND ( 'NONE', #3184, .T. ) ;
#6568=ORIENTED_EDGE ( 'NONE', *, *, #3707, .T. ) ;
#6577=ORIENTED_EDGE ( 'NONE', *, *, #8485, .T. ) ;
#6579=EDGE_CURVE ( 'NONE', #2446, #3145, #968, .T. ) ;
#6590=DIRECTION ( 'NONE',  ( 1.000000000000000000, 0.000000000000000000, 0.000000000000000000 ) ) ;
#6608=DIRECTION ( 'NONE',  ( 1.000000000000000000, 0.000000000000000000, 0.000000000000000000 ) ) ;
#6621=EDGE_CURVE ( 'NONE', #5056, #11949, #8196, .T. ) ;
#6636=CARTESIAN_POINT ( 'NONE',  ( 1.567478505476134606E-15, 4.618802153517012066, -5.000000000000000000 ) ) ;
#6646=CARTESIAN_POINT ( 'NONE',  ( 3.999999999999999112, 1.941961291383486277, -0.3515519931180248192 ) ) ;
#6654=ORIENTED_EDGE ( 'NONE', *, *, #6128, .T. ) ;
#6672=CARTESIAN_POINT ( 'NONE',  ( -2.100000000000000089, 2.571758278209441957E-16, -5.000000000000000000 ) ) ;
#6679=EDGE_LOOP ( 'NONE', ( #5819, #1427, #9988, #1263 ) ) ;
#6684=CARTESIAN_POINT ( 'NONE',  ( -2.725741868435985094, 3.045094352034055429, -3.220599429844047012 ) ) ;
#6689=ORIENTED_EDGE ( 'NONE', *, *, #2028, .F. ) ;
#6695=CARTESIAN_POINT ( 'NONE',  ( 0.000000000000000000, 0.000000000000000000, -0.3080913168122742518 ) ) ;
#6701=CARTESIAN_POINT ( 'NONE',  ( 4.000000000000000000, 2.309401076758497151, -5.000000000000000000 ) ) ;
#6708=CARTESIAN_POINT ( 'NONE',  ( 3.999999999999999112, -0.7890432684750902093, -0.04868663549882291247 ) ) ;
#6720=ORIENTED_EDGE ( 'NONE', *, *, #11684, .F. ) ;
#6739=EDGE_CURVE ( 'NONE', #6877, #7500, #12869, .T. ) ;
#6741=ORIENTED_EDGE ( 'NONE', *, *, #5278, .T. ) ;
#6756=ORIENTED_EDGE ( 'NONE', *, *, #6579, .T. ) ;
#6763=DIRECTION ( 'NONE',  ( -0.000000000000000000, -0.000000000000000000, 1.000000000000000000 ) ) ;
#6771=VECTOR ( 'NONE', #12941, 1000.000000000000000 ) ;
#6779=SHAPE_REPRESENTATION ( 'hex flange nut gradea_iso_ISO - 4161 - M5 - N', ( #9440 ), #2159 ) ;
#6799=CARTESIAN_POINT ( 'NONE',  ( -4.000000000000000000, 2.309401076758498483, -3.433295621305379353 ) ) ;
#6804=CARTESIAN_POINT ( 'NONE',  ( 4.198928548860774157, -0.8158838809860124996, -3.526471437616918170 ) ) ;
#6809=EDGE_CURVE ( 'NONE', #10412, #3419, #3526, .T. ) ;
#6819=CARTESIAN_POINT ( 'NONE',  ( 1.999999999999998224, -3.464101615137772594, -3.142992957459239012 ) ) ;
#6855=CARTESIAN_POINT ( 'NONE',  ( 4.000000000000000000, 2.309401076758497151, -5.000000000000000000 ) ) ;
#6877=VERTEX_POINT ( 'NONE', #5122 ) ;
#6880=AXIS2_PLACEMENT_3D ( 'NONE', #3069, #7572, #5351 ) ;
#6883=VERTEX_POINT ( 'NONE', #9705 ) ;
#6886=CARTESIAN_POINT ( 'NONE',  ( -0.3461262719736137305, 4.658553426539289610, -3.671615880910373608 ) ) ;
#6889=CARTESIAN_POINT ( 'NONE',  ( 4.203935335434060505, 1.640780671294165272, -3.598452447879202598 ) ) ;
#6915=CARTESIAN_POINT ( 'NONE',  ( -4.000000000000000000, 2.309401076758498483, -5.000000000000000000 ) ) ;
#6916=EDGE_CURVE ( 'NONE', #12480, #1630, #6089, .T. ) ;
#6949=CARTESIAN_POINT ( 'NONE',  ( -0.3198814748697807464, -4.434118497892185040, -0.3507732604232532969 ) ) ;
#6958=CARTESIAN_POINT ( 'NONE',  ( -4.207491450040567571, 2.029819825146470524, -3.671670828759566074 ) ) ;
#6960=B_SPLINE_CURVE_WITH_KNOTS ( 'NONE', 3,
 ( #5467, #14468, #11963, #2826, #11208, #1856, #6646, #11139 ),
 .UNSPECIFIED., .F., .F.,
 ( 4, 2, 2, 4 ),
 ( 0.005725059856848645212, 0.006314084072593634418, 0.006903108288338624492, 0.008081156719828603771 ),
 .UNSPECIFIED. ) ;
#6969=FACE_OUTER_BOUND ( 'NONE', #3059, .T. ) ;
#6986=ADVANCED_FACE ( 'NONE', ( #3691 ), #12181, .F. ) ;
#6993=CARTESIAN_POINT ( 'NONE',  ( 2.742827927723449299, 3.035229711104609596, -3.433252694550591233 ) ) ;
#7004=ORIENTED_EDGE ( 'NONE', *, *, #11417, .F. ) ;
#7024=ADVANCED_BREP_SHAPE_REPRESENTATION ( '', ( #12291, #9440 ), #2159 ) ;
#7032=CARTESIAN_POINT ( 'NONE',  ( 4.000000000000000000, -2.309401076758514915, -5.000000000000000000 ) ) ;
#7035=CARTESIAN_POINT ( 'NONE',  ( -2.804994570502171047, -3.229033611042465335, -3.526374918436838701 ) ) ;
#7056=EDGE_CURVE ( 'NONE', #3815, #4304, #5400, .T. ) ;
#7057=AXIS2_PLACEMENT_3D ( 'NONE', #3295, #3219, #8769 ) ;
#7058=VECTOR ( 'NONE', #12003, 1000.000000000000000 ) ;
#7067=CONICAL_SURFACE ( 'NONE', #2361, 4.000000000000000000, 0.8911886515913786111 ) ;
#7068=CIRCLE ( 'NONE', #4489, 4.000000000000000000 ) ;
#7080=ORIENTED_EDGE ( 'NONE', *, *, #9309, .T. ) ;
#7097=ADVANCED_FACE ( 'NONE', ( #6199 ), #8155, .F. ) ;
#7146=CARTESIAN_POINT ( 'NONE',  ( 0.6666666666666689611, 4.233901974057261874, -3.300726591567082480 ) ) ;
#7182=DIRECTION ( 'NONE',  ( -0.000000000000000000, 0.000000000000000000, -1.000000000000000000 ) ) ;
#7192=CARTESIAN_POINT ( 'NONE',  ( 0.6640947660595348800, -4.471078309994175548, -3.602146406945708090 ) ) ;
#7197=EDGE_CURVE ( 'NONE', #7500, #8478, #13715, .T. ) ;
#7220=CARTESIAN_POINT ( 'NONE',  ( 8.673617379884035472E-16, 4.618802153517012954, -5.000000000000000000 ) ) ;
#7260=CARTESIAN_POINT ( 'NONE',  ( 2.500000000000000444, 0.000000000000000000, -5.000000000000000888 ) ) ;
#7284=B_SPLINE_CURVE_WITH_KNOTS ( 'NONE', 3,
 ( #3944, #11539, #5126, #8431, #8140, #12647 ),
 .UNSPECIFIED., .F., .F.,
 ( 4, 2, 4 ),
 ( -3.640115492410698714E-06, 0.0002066546034003381217, 0.0004169493222930869755 ),
 .UNSPECIFIED. ) ;
#7288=EDGE_CURVE ( 'NONE', #4304, #3815, #11766, .T. ) ;
#7300=CIRCLE ( 'NONE', #11068, 5.560781378645573980 ) ;
#7329=CARTESIAN_POINT ( 'NONE',  ( -2.000000000000007550, -3.464101615137749945, 0.000000000000000000 ) ) ;
#7333=CARTESIAN_POINT ( 'NONE',  ( -3.510273485745307287, -2.827716139362669967, -3.610536846335890004 ) ) ;
#7338=CARTESIAN_POINT ( 'NONE',  ( 3.455068668934414777, -2.624017327439094327, -3.316620875263732504 ) ) ;
#7339=ORIENTED_EDGE ( 'NONE', *, *, #8485, .F. ) ;
#7359=VECTOR ( 'NONE', #8167, 1000.000000000000000 ) ;
#7362=PRODUCT_DEFINITION_FORMATION_WITH_SPECIFIED_SOURCE ( 'ANY', '', #2394, .NOT_KNOWN. ) ;
#7380=ORIENTED_EDGE ( 'NONE', *, *, #2609, .T. ) ;
#7393=B_SPLINE_CURVE_WITH_KNOTS ( 'NONE', 3,
 ( #14431, #8459, #5016, #11018, #1529, #9513 ),
 .UNSPECIFIED., .F., .F.,
 ( 4, 2, 4 ),
 ( 0.000000000000000000, 0.0002095117440864783663, 0.0004190234881729567326 ),
 .UNSPECIFIED. ) ;
#7401=FACE_OUTER_BOUND ( 'NONE', #10802, .T. ) ;
#7409=CARTESIAN_POINT ( 'NONE',  ( 0.000000000000000000, 0.000000000000000000, -5.000000000000000888 ) ) ;
#7427=CARTESIAN_POINT ( 'NONE',  ( 0.000000000000000000, 0.000000000000000000, -4.000000000000000000 ) ) ;
#7436=CARTESIAN_POINT ( 'NONE',  ( 2.687328764639642653, -3.067272167851299969, -0.05923475698271395140 ) ) ;
#7458=ORIENTED_EDGE ( 'NONE', *, *, #6365, .T. ) ;
#7473=VECTOR ( 'NONE', #3607, 1000.000000000000000 ) ;
#7477=( NAMED_UNIT ( * ) SI_UNIT ( $, .STERADIAN. ) SOLID_ANGLE_UNIT ( ) );
#7484=AXIS2_PLACEMENT_3D ( 'NONE', #11693, #11555, #11763 ) ;
#7490=DIRECTION ( 'NONE',  ( -0.000000000000000000, -0.000000000000000000, 1.000000000000000000 ) ) ;
#7499=DIRECTION ( 'NONE',  ( -1.000000000000000000, 0.000000000000000000, 0.000000000000000000 ) ) ;
#7500=VERTEX_POINT ( 'NONE', #2397 ) ;
#7537=ORIENTED_EDGE ( 'NONE', *, *, #3048, .F. ) ;
#7572=DIRECTION ( 'NONE',  ( 0.000000000000000000, 0.000000000000000000, -1.000000000000000000 ) ) ;
#7575=CARTESIAN_POINT ( 'NONE',  ( 0.1756481739660539498, -4.720212674038995360, -3.469390959564070620 ) ) ;
#7586=DIRECTION ( 'NONE',  ( -0.000000000000000000, -0.000000000000000000, 1.000000000000000000 ) ) ;
#7616=AXIS2_PLACEMENT_3D ( 'NONE', #6915, #11474, #1369 ) ;
#7619=( BOUNDED_SURFACE ( )  B_SPLINE_SURFACE ( 3, 2, ( 
 ( #12190, #7782, #11390 ),
 ( #10635, #9032, #12572 ),
 ( #1280, #10552, #12845 ),
 ( #5778, #4682, #9175 ),
 ( #5631, #13464, #6889 ),
 ( #513, #6047, #11720 ) ),
 .UNSPECIFIED., .F., .F., .F. ) 
 B_SPLINE_SURFACE_WITH_KNOTS ( ( 4, 2, 4 ),
 ( 3, 3 ),
 ( 0.02027065861071770947, 0.02273072267836921331, 0.02519078674602071716 ),
 ( 0.000000000000000000, 1.000000000000000000 ),
 .UNSPECIFIED. ) 
 GEOMETRIC_REPRESENTATION_ITEM ( )  RATIONAL_B_SPLINE_SURFACE ( (
 ( 1.000000000000000000, 0.8047781708337304885, 1.000000000000000000),
 ( 1.000000000000000000, 0.8123765190705307671, 1.000000000000000000),
 ( 1.000000000000000000, 0.8190656277163975707, 1.000000000000000000),
 ( 1.000000000000000000, 0.8192366903512159348, 1.000000000000000000),
 ( 1.000000000000000000, 0.8126138454302893610, 1.000000000000000000),
 ( 1.000000000000000000, 0.8047712246031417660, 1.000000000000000000) ) ) 
 REPRESENTATION_ITEM ( '' )  SURFACE ( )  );
#7627=ADVANCED_FACE ( 'NONE', ( #6969 ), #12127, .F. ) ;
#7636=SURFACE_STYLE_USAGE ( .BOTH. , #3133 ) ;
#7644=CARTESIAN_POINT ( 'NONE',  ( -3.355112389629170799, 2.681727112203152963, -0.2256878752776689534 ) ) ;
#7645=EDGE_CURVE ( 'NONE', #4981, #10556, #7300, .T. ) ;
#7651=CARTESIAN_POINT ( 'NONE',  ( -1.257172072275743346, 3.892973519171203378, -3.433252694550776862 ) ) ;
#7652=CARTESIAN_POINT ( 'NONE',  ( -0.6810597143197697489, -4.461075778259609770, -3.598441714920717516 ) ) ;
#7660=ORIENTED_EDGE ( 'NONE', *, *, #5219, .T. ) ;
#7674=VERTEX_POINT ( 'NONE', #7260 ) ;
#7686=ORIENTED_EDGE ( 'NONE', *, *, #6202, .T. ) ;
#7706=CARTESIAN_POINT ( 'NONE',  ( -2.687328764639638656, 3.067272167851286202, -0.05923475698270370959 ) ) ;
#7712=FACE_OUTER_BOUND ( 'NONE', #4326, .T. ) ;
#7715=EDGE_CURVE ( 'NONE', #4117, #3851, #7284, .T. ) ;
#7763=VECTOR ( 'NONE', #362, 1000.000000000000114 ) ;
#7774=EDGE_CURVE ( 'NONE', #9996, #2446, #11669, .T. ) ;
#7782=CARTESIAN_POINT ( 'NONE',  ( 4.000000000000000000, -2.471525695159793035, -3.686886880705770864 ) ) ;
#7798=CARTESIAN_POINT ( 'NONE',  ( 0.000000000000000000, 0.000000000000000000, 0.000000000000000000 ) ) ;
#7860=CONICAL_SURFACE ( 'NONE', #9031, 5.560781378645573980, 1.221730476396046816 ) ;
#7911=EDGE_CURVE ( 'NONE', #1238, #4931, #5772, .T. ) ;
#7914=CARTESIAN_POINT ( 'NONE',  ( -4.000000000000000888, -1.539600717839011201, -3.300726591567081591 ) ) ;
#7920=CARTESIAN_POINT ( 'NONE',  ( 1.411581201560190495E-15, 4.862606272033091592, -3.745885042887436622 ) ) ;
#7983=CARTESIAN_POINT ( 'NONE',  ( 4.204015924366189871, -1.626724848190933548, -3.610627190413393084 ) ) ;
#7986=CARTESIAN_POINT ( 'NONE',  ( -4.204015924366189871, 1.626724848190922446, -3.610627190413390419 ) ) ;
#8005=AXIS2_PLACEMENT_3D ( 'NONE', #13785, #6763, #5666 ) ;
#8016=CARTESIAN_POINT ( 'NONE',  ( 2.500000000000000444, 0.000000000000000000, -25.03750572909317285 ) ) ;
#8017=PLANE ( 'NONE',  #7616 ) ;
#8046=CARTESIAN_POINT ( 'NONE',  ( 4.203833317240879275, 1.627343821129582979, -3.597273115243889929 ) ) ;
#8049=CARTESIAN_POINT ( 'NONE',  ( 4.211140560182196957, -2.431303136016555122, -3.745885042887436622 ) ) ;
#8056=CARTESIAN_POINT ( 'NONE',  ( -4.000000000000000000, -7.806255641895631925E-15, -3.142992957459232350 ) ) ;
#8128=LINE ( 'NONE', #3931, #12998 ) ;
#8140=CARTESIAN_POINT ( 'NONE',  ( -4.000000000000003553, 2.309401076758496263, -3.504269196027868905 ) ) ;
#8151=CARTESIAN_POINT ( 'NONE',  ( -2.742827927723112236, -3.035229711105190464, -3.433252694550595230 ) ) ;
#8155=( BOUNDED_SURFACE ( )  B_SPLINE_SURFACE ( 3, 2, ( 
 ( #11925, #3767, #8396 ),
 ( #6037, #14025, #10541 ),
 ( #415, #8327, #8474 ),
 ( #13953, #10623, #570 ),
 ( #5093, #3846, #10759 ),
 ( #637, #5161, #10696 ) ),
 .UNSPECIFIED., .F., .F., .T. ) 
 B_SPLINE_SURFACE_WITH_KNOTS ( ( 4, 2, 4 ),
 ( 3, 3 ),
 ( 0.02027752710269158445, 0.02273781595091097299, 0.02519810479913036153 ),
 ( 0.000000000000000000, 1.000000000000000000 ),
 .UNSPECIFIED. ) 
 GEOMETRIC_REPRESENTATION_ITEM ( )  RATIONAL_B_SPLINE_SURFACE ( (
 ( 1.000000000000000000, 0.8047781431712808242, 1.000000000000000000),
 ( 1.000000000000000000, 0.8123773247083928561, 1.000000000000000000),
 ( 1.000000000000000000, 0.8190670192154906326, 1.000000000000000000),
 ( 1.000000000000000000, 0.8192353552912178261, 1.000000000000000000),
 ( 1.000000000000000000, 0.8126132098226825917, 1.000000000000000000),
 ( 1.000000000000000000, 0.8047712465856394770, 1.000000000000000000) ) ) 
 REPRESENTATION_ITEM ( '' )  SURFACE ( )  );
#8161=CARTESIAN_POINT ( 'NONE',  ( -4.000000000000000000, 0.000000000000000000, 0.000000000000000000 ) ) ;
#8167=DIRECTION ( 'NONE',  ( 0.000000000000000000, 0.000000000000000000, 1.000000000000000000 ) ) ;
#8183=CARTESIAN_POINT ( 'NONE',  ( 2.000000000000008882, 3.464101615137749945, 0.000000000000000000 ) ) ;
#8195=ORIENTED_EDGE ( 'NONE', *, *, #13842, .T. ) ;
#8196=B_SPLINE_CURVE_WITH_KNOTS ( 'NONE', 3,
 ( #11244, #1056, #13472, #5565, #10065, #13543 ),
 .UNSPECIFIED., .F., .F.,
 ( 4, 2, 4 ),
 ( 0.002365888236227977302, 0.003551327329835078910, 0.004736766423442180518 ),
 .UNSPECIFIED. ) ;
#8207=CARTESIAN_POINT ( 'NONE',  ( -6.259644161404859044E-16, -4.618802153517026277, -3.504271511727133248 ) ) ;
#8215=CARTESIAN_POINT ( 'NONE',  ( 1.360585162435110629, -4.061296242128317857, -3.505054077164905024 ) ) ;
#8242=CARTESIAN_POINT ( 'NONE',  ( 4.000000000000000000, 2.309401076758497151, -3.433295621305379353 ) ) ;
#8248=CARTESIAN_POINT ( 'NONE',  ( 4.175002511812151873, 2.208363329454889445, -3.469254087858244073 ) ) ;
#8263=CARTESIAN_POINT ( 'NONE',  ( -4.024497503033714452, -2.323544716729502468, -3.572167766733752803 ) ) ;
#8264=CONICAL_SURFACE ( 'NONE', #9932, 4.000000000000000000, 0.8911886515913786111 ) ;
#8276=ORIENTED_EDGE ( 'NONE', *, *, #8287, .F. ) ;
#8287=EDGE_CURVE ( 'NONE', #4931, #6458, #13354, .T. ) ;
#8292=FACE_BOUND ( 'NONE', #5355, .T. ) ;
#8313=ORIENTED_EDGE ( 'NONE', *, *, #11654, .F. ) ;
#8316=FACE_OUTER_BOUND ( 'NONE', #5372, .T. ) ;
#8327=CARTESIAN_POINT ( 'NONE',  ( -4.000000000000000000, 0.8576368993457507139, -3.433240632782198709 ) ) ;
#8341=B_SPLINE_CURVE_WITH_KNOTS ( 'NONE', 3,
 ( #12405, #1113, #6804, #7983, #12343, #13755 ),
 .UNSPECIFIED., .F., .F.,
 ( 4, 2, 4 ),
 ( 0.002452478801916361129, 0.003676905084148001344, 0.004901331366379641126 ),
 .UNSPECIFIED. ) ;
#8358=CARTESIAN_POINT ( 'NONE',  ( 0.000000000000000000, 0.000000000000000000, 0.000000000000000000 ) ) ;
#8365=DIRECTION ( 'NONE',  ( -0.000000000000000000, -0.000000000000000000, 1.000000000000000000 ) ) ;
#8366=EDGE_LOOP ( 'NONE', ( #965, #154, #14125, #12886 ) ) ;
#8396=CARTESIAN_POINT ( 'NONE',  ( -4.211399284164270895, 2.459729995988205964, -3.751162237960538715 ) ) ;
#8431=CARTESIAN_POINT ( 'NONE',  ( -4.024497503033714452, 2.323544716729487813, -3.572167766733750582 ) ) ;
#8434=CARTESIAN_POINT ( 'NONE',  ( -4.000000000000000000, 1.941961291383472732, -0.3515519931180205448 ) ) ;
#8443=CARTESIAN_POINT ( 'NONE',  ( -4.000000000000000000, 0.000000000000000000, 0.000000000000000000 ) ) ;
#8459=CARTESIAN_POINT ( 'NONE',  ( 3.999999999999999112, 2.309401076758497595, -3.504271511727124366 ) ) ;
#8468=CARTESIAN_POINT ( 'NONE',  ( -3.349226789952655547, -2.685125164760744809, -0.2236248678334863682 ) ) ;
#8474=CARTESIAN_POINT ( 'NONE',  ( -4.197477534772231955, 0.8522413273724368521, -3.505042416683225692 ) ) ;
#8478=VERTEX_POINT ( 'NONE', #1542 ) ;
#8484=CONICAL_SURFACE ( 'NONE', #4245, 2.059999999999998721, 0.9599310885968738161 ) ;
#8485=EDGE_CURVE ( 'NONE', #3563, #2314, #8488, .T. ) ;
#8488=B_SPLINE_CURVE_WITH_KNOTS ( 'NONE', 3,
 ( #3629, #8046, #11646, #1396 ),
 .UNSPECIFIED., .F., .F.,
 ( 4, 4 ),
 ( 0.000000000000000000, 0.002452478801916361129 ),
 .UNSPECIFIED. ) ;
#8505=FACE_OUTER_BOUND ( 'NONE', #1905, .T. ) ;
#8512=DIRECTION ( 'NONE',  ( -1.000000000000000000, 0.000000000000000000, 0.000000000000000000 ) ) ;
#8521=ORIENTED_EDGE ( 'NONE', *, *, #3377, .T. ) ;
#8550=CARTESIAN_POINT ( 'NONE',  ( -4.000000000000000000, -2.309401076758512694, -5.000000000000000000 ) ) ;
#8573=PRODUCT_CONTEXT ( 'NONE', #1022, 'mechanical' ) ;
#8577=DIRECTION ( 'NONE',  ( 1.224646799147353207E-16, 1.000000000000000000, 0.000000000000000000 ) ) ;
#8578=DIRECTION ( 'NONE',  ( -0.000000000000000000, -0.000000000000000000, 1.000000000000000000 ) ) ;
#8615=CARTESIAN_POINT ( 'NONE',  ( 2.000000000000005329, -3.464101615137751722, 0.000000000000000000 ) ) ;
#8644=DIRECTION ( 'NONE',  ( 0.8660254037844374864, -0.5000000000000018874, 0.000000000000000000 ) ) ;
#8670=DIRECTION ( 'NONE',  ( -1.000000000000000000, 0.000000000000000000, 0.000000000000000000 ) ) ;
#8691=LINE ( 'NONE', #8550, #7058 ) ;
#8720=ADVANCED_FACE ( 'NONE', ( #2180 ), #8264, .T. ) ;
#8721=CIRCLE ( 'NONE', #7057, 2.500000000000000444 ) ;
#8731=ORIENTED_EDGE ( 'NONE', *, *, #4385, .T. ) ;
#8733=CIRCLE ( 'NONE', #14167, 2.500000000000000444 ) ;
#8745=EDGE_CURVE ( 'NONE', #2446, #9530, #2469, .T. ) ;
#8746=CARTESIAN_POINT ( 'NONE',  ( -3.680118525130244400, 2.494084732383327285, -0.3507732604232449702 ) ) ;
#8747=B_SPLINE_CURVE_WITH_KNOTS ( 'NONE', 3,
 ( #11194, #13625, #4567, #5662 ),
 .UNSPECIFIED., .F., .F.,
 ( 4, 4 ),
 ( 0.000000000000000000, 0.002452478801916376308 ),
 .UNSPECIFIED. ) ;
#8751=AXIS2_PLACEMENT_3D ( 'NONE', #5985, #2804, #11655 ) ;
#8755=VECTOR ( 'NONE', #3373, 1000.000000000000000 ) ;
#8765=ORIENTED_EDGE ( 'NONE', *, *, #7774, .T. ) ;
#8769=DIRECTION ( 'NONE',  ( -1.000000000000000000, 0.000000000000000000, 0.000000000000000000 ) ) ;
#8823=CARTESIAN_POINT ( 'NONE',  ( 2.000000000000008882, 3.464101615137749945, 0.000000000000000000 ) ) ;
#8837=VERTEX_POINT ( 'NONE', #4471 ) ;
#8875=CARTESIAN_POINT ( 'NONE',  ( -4.000000000000000000, 2.309401076758498483, -3.433295621305379353 ) ) ;
#8877=PLANE ( 'NONE',  #5402 ) ;
#8878=CARTESIAN_POINT ( 'NONE',  ( -2.855764796983342624, 2.970025579236414082, -0.09382832055445475272 ) ) ;
#8918=CARTESIAN_POINT ( 'NONE',  ( 1.393927851585479161, -4.043713361053543842, -3.526374918436840922 ) ) ;
#8927=DIRECTION ( 'NONE',  ( 1.000000000000000000, 0.000000000000000000, 0.000000000000000000 ) ) ;
#8931=ORIENTED_EDGE ( 'NONE', *, *, #7197, .F. ) ;
#8981=ORIENTED_EDGE ( 'NONE', *, *, #13418, .F. ) ;
#8983=EDGE_CURVE ( 'NONE', #10969, #2440, #765, .T. ) ;
#8998=CARTESIAN_POINT ( 'NONE',  ( 4.000000000000000000, -1.560351142792952617, -0.2242961665059816367 ) ) ;
#9001=DIRECTION ( 'NONE',  ( -1.000000000000000000, 0.000000000000000000, 0.000000000000000000 ) ) ;
#9003=FACE_OUTER_BOUND ( 'NONE', #1240, .T. ) ;
#9031=AXIS2_PLACEMENT_3D ( 'NONE', #7427, #9788, #10002 ) ;
#9032=CARTESIAN_POINT ( 'NONE',  ( 4.000000000000000000, -1.677850389431204459, -3.535268758346977513 ) ) ;
#9033=( BOUNDED_SURFACE ( )  B_SPLINE_SURFACE ( 3, 2, ( 
 ( #10598, #5008, #13844 ),
 ( #9571, #2638, #14071 ),
 ( #2851, #8151, #11846 ),
 ( #4790, #12658, #6021 ),
 ( #1960, #9787, #7652 ),
 ( #7575, #773, #14146 ) ),
 .UNSPECIFIED., .F., .F., .F. ) 
 B_SPLINE_SURFACE_WITH_KNOTS ( ( 4, 2, 4 ),
 ( 3, 3 ),
 ( 0.02032853247518126918, 0.02278863295364821906, 0.02524873343211516893 ),
 ( 0.000000000000000000, 1.000000000000000000 ),
 .UNSPECIFIED. ) 
 GEOMETRIC_REPRESENTATION_ITEM ( )  RATIONAL_B_SPLINE_SURFACE ( (
 ( 1.000000000000000000, 0.8047781615896838492, 1.000000000000000000),
 ( 1.000000000000000000, 0.8123767586288186404, 1.000000000000000000),
 ( 1.000000000000000000, 0.8190662415565814758, 1.000000000000000000),
 ( 1.000000000000000000, 0.8192361015667604107, 1.000000000000000000),
 ( 1.000000000000000000, 0.8126135807104967190, 1.000000000000000000),
 ( 1.000000000000000000, 0.8047712338318580017, 1.000000000000000000) ) ) 
 REPRESENTATION_ITEM ( '' )  SURFACE ( )  );
#9038=B_SPLINE_CURVE_WITH_KNOTS ( 'NONE', 3,
 ( #2119, #9963, #8998, #6708, #1161, #3454 ),
 .UNSPECIFIED., .F., .F.,
 ( 4, 2, 4 ),
 ( 0.003358874760055551890, 0.004541967308452098118, 0.005725059856848645212 ),
 .UNSPECIFIED. ) ;
#9067=CARTESIAN_POINT ( 'NONE',  ( 0.6937372685066666156, -4.453844082567737672, -3.610536846335894445 ) ) ;
#9090=EDGE_CURVE ( 'NONE', #1630, #3851, #6057, .T. ) ;
#9104=CARTESIAN_POINT ( 'NONE',  ( -4.141042297810615835, 2.227970268150415656, -3.687027686973619822 ) ) ;
#9123=ORIENTED_EDGE ( 'NONE', *, *, #9139, .F. ) ;
#9133=AXIS2_PLACEMENT_3D ( 'NONE', #614, #12065, #14287 ) ;
#9139=EDGE_CURVE ( 'NONE', #4117, #12480, #2356, .T. ) ;
#9158=EDGE_CURVE ( 'NONE', #2314, #2790, #8341, .T. ) ;
#9163=AXIS2_PLACEMENT_3D ( 'NONE', #12542, #2434, #12682 ) ;
#9175=CARTESIAN_POINT ( 'NONE',  ( 4.197310751797292738, 0.8178363989516252985, -3.502498386812444409 ) ) ;
#9186=ORIENTED_EDGE ( 'NONE', *, *, #6399, .T. ) ;
#9237=CARTESIAN_POINT ( 'NONE',  ( 2.682243648011666703, 3.070208061305304881, -0.04852650426601266831 ) ) ;
#9245=CARTESIAN_POINT ( 'NONE',  ( -1.312671235360383548, -3.860931062424228788, -0.05923475698271369466 ) ) ;
#9264=CARTESIAN_POINT ( 'NONE',  ( -2.449848172108560540, -3.432307619358754724, -3.503702292528910078 ) ) ;
#9282=CARTESIAN_POINT ( 'NONE',  ( 1.655952806101427033, -3.662737355149048302, -1.182683869819604841E-14 ) ) ;
#9289=CARTESIAN_POINT ( 'NONE',  ( -4.000000000000000000, -0.7890432684750890990, -0.04868663549882315533 ) ) ;
#9295=CARTESIAN_POINT ( 'NONE',  ( 1.390230914382191596, 4.043987460488659202, -3.502507215260488582 ) ) ;
#9306=DIRECTION ( 'NONE',  ( 0.000000000000000000, 0.000000000000000000, -1.000000000000000000 ) ) ;
#9309=EDGE_CURVE ( 'NONE', #3851, #2440, #8128, .T. ) ;
#9336=CARTESIAN_POINT ( 'NONE',  ( 2.725741868436127202, -3.045094352033990148, -3.220599429844051453 ) ) ;
#9346=DIRECTION ( 'NONE',  ( -1.000000000000000000, 0.000000000000000000, 0.000000000000000000 ) ) ;
#9368=ORIENTED_EDGE ( 'NONE', *, *, #8745, .F. ) ;
#9373=CARTESIAN_POINT ( 'NONE',  ( 0.000000000000000000, 0.000000000000000000, -4.974599999999998801 ) ) ;
#9404=CARTESIAN_POINT ( 'NONE',  ( -1.391697335622809950, -4.043246145443391448, -3.503898532754372575 ) ) ;
#9407=DIRECTION ( 'NONE',  ( 1.000000000000000000, 0.000000000000000000, 0.000000000000000000 ) ) ;
#9440=AXIS2_PLACEMENT_3D ( 'NONE', #4347, #14302, #6417 ) ;
#9475=CARTESIAN_POINT ( 'NONE',  ( 3.999999999999999112, -1.539600717839012978, -3.300726591567080703 ) ) ;
#9479=MECHANICAL_DESIGN_GEOMETRIC_PRESENTATION_REPRESENTATION('',(#14429),#3110);
#9481=ORIENTED_EDGE ( 'NONE', *, *, #6365, .F. ) ;
#9510=EDGE_CURVE ( 'NONE', #1371, #10838, #2114, .T. ) ;
#9513=CARTESIAN_POINT ( 'NONE',  ( 4.211140560182196957, 2.431303136016536470, -3.745885042887433514 ) ) ;
#9530=VERTEX_POINT ( 'NONE', #5478 ) ;
#9555=PLANE ( 'NONE',  #1367 ) ;
#9562=ORIENTED_EDGE ( 'NONE', *, *, #7056, .T. ) ;
#9571=CARTESIAN_POINT ( 'NONE',  ( -3.472371940586054251, -2.614027278893156669, -3.320322319202162031 ) ) ;
#9572=CYLINDRICAL_SURFACE ( 'NONE', #13269, 2.500000000000000444 ) ;
#9579=CARTESIAN_POINT ( 'NONE',  ( 0.000000000000000000, 0.000000000000000000, 0.000000000000000000 ) ) ;
#9603=AXIS2_PLACEMENT_3D ( 'NONE', #112, #11366, #8927 ) ;
#9608=DIRECTION ( 'NONE',  ( -1.000000000000000000, 1.224646799147352714E-16, 0.000000000000000000 ) ) ;
#9610=LINE ( 'NONE', #1778, #11511 ) ;
#9622=CARTESIAN_POINT ( 'NONE',  ( 1.411581201560190495E-15, 4.862606272033091592, -3.745885042887436622 ) ) ;
#9627=CARTESIAN_POINT ( 'NONE',  ( -2.000000000000002665, -3.464101615137770374, -3.142992957459237680 ) ) ;
#9673=CARTESIAN_POINT ( 'NONE',  ( -4.000000000000000000, 2.309401076758498483, -3.433295621305379353 ) ) ;
#9689=CARTESIAN_POINT ( 'NONE',  ( -5.384454397937118664, 6.594054843588581554E-16, -4.484454397937119197 ) ) ;
#9705=CARTESIAN_POINT ( 'NONE',  ( -4.211140560182196957, -2.431303136016552013, -3.745885042887436178 ) ) ;
#9726=CIRCLE ( 'NONE', #751, 2.499999999999999556 ) ;
#9737=CARTESIAN_POINT ( 'NONE',  ( 3.680118525130245732, -2.494084732383344605, -0.3507732604232533524 ) ) ;
#9748=CLOSED_SHELL ( 'NONE', ( #13335, #13869, #6487, #12147, #5479, #2280, #6986, #2799, #11907, #3306, #1700, #2523, #11955, #1334, #998, #13373, #14490, #11508, #3061, #8720, #10124, #11172, #4528, #6379, #7627, #7097, #4986, #1100, #856, #4408, #9799, #12043 ) ) ;
#9754=ORIENTED_EDGE ( 'NONE', *, *, #14141, .F. ) ;
#9777=CARTESIAN_POINT ( 'NONE',  ( -0.6666666666666666297, -4.233901974057276973, -3.300726591567087365 ) ) ;
#9784=DIRECTION ( 'NONE',  ( -0.000000000000000000, 0.000000000000000000, -1.000000000000000000 ) ) ;
#9787=CARTESIAN_POINT ( 'NONE',  ( -0.5636800770129166693, -4.293361309317430319, -3.531542292955206275 ) ) ;
#9788=DIRECTION ( 'NONE',  ( 0.000000000000000000, 0.000000000000000000, -1.000000000000000000 ) ) ;
#9799=ADVANCED_FACE ( 'NONE', ( #10331 ), #1894, .F. ) ;
#9850=CARTESIAN_POINT ( 'NONE',  ( 0.000000000000000000, 0.000000000000000000, 0.000000000000000000 ) ) ;
#9915=FILL_AREA_STYLE ('',( #6294 ) ) ;
#9932=AXIS2_PLACEMENT_3D ( 'NONE', #7798, #13113, #7499 ) ;
#9937=ORIENTED_EDGE ( 'NONE', *, *, #7645, .F. ) ;
#9963=CARTESIAN_POINT ( 'NONE',  ( 4.000000000000000000, -1.942223658245635809, -0.3516579909967643691 ) ) ;
#9976=DIRECTION ( 'NONE',  ( 1.000000000000000000, 0.000000000000000000, 0.000000000000000000 ) ) ;
#9977=CARTESIAN_POINT ( 'NONE',  ( 4.211140560182196957, 2.431303136016536470, -3.745885042887433514 ) ) ;
#9988=ORIENTED_EDGE ( 'NONE', *, *, #12408, .F. ) ;
#9996=VERTEX_POINT ( 'NONE', #12394 ) ;
#9999=CARTESIAN_POINT ( 'NONE',  ( 1.312671235360372224, 3.860931062424219462, -0.05923475698270440348 ) ) ;
#10002=DIRECTION ( 'NONE',  ( -1.000000000000000000, 0.000000000000000000, 0.000000000000000000 ) ) ;
#10010=ORIENTED_EDGE ( 'NONE', *, *, #7715, .F. ) ;
#10065=CARTESIAN_POINT ( 'NONE',  ( -0.3208286057739654917, 4.433571671609680465, -0.3503314178412548774 ) ) ;
#10083=AXIS2_PLACEMENT_3D ( 'NONE', #742, #4152, #8644 ) ;
#10115=DIRECTION ( 'NONE',  ( 0.9396926207859138680, 1.150791560227856926E-16, -0.3420201433256536139 ) ) ;
#10120=ORIENTED_EDGE ( 'NONE', *, *, #12700, .T. ) ;
#10121=VECTOR ( 'NONE', #1080, 999.9999999999998863 ) ;
#10124=ADVANCED_FACE ( 'NONE', ( #12918 ), #6149, .T. ) ;
#10142=CARTESIAN_POINT ( 'NONE',  ( -3.522875095019672109, 2.820352903225427532, -3.598441714920591394 ) ) ;
#10144=( NAMED_UNIT ( * ) SI_UNIT ( $, .STERADIAN. ) SOLID_ANGLE_UNIT ( ) );
#10185=DIRECTION ( 'NONE',  ( 0.000000000000000000, 0.000000000000000000, -1.000000000000000000 ) ) ;
#10242=CARTESIAN_POINT ( 'NONE',  ( -4.000000000000000000, -1.942223658245633811, -0.3516579909967644246 ) ) ;
#10243=EDGE_CURVE ( 'NONE', #10412, #740, #3095, .T. ) ;
#10253=EDGE_CURVE ( 'NONE', #6883, #9996, #4659, .T. ) ;
#10271=CARTESIAN_POINT ( 'NONE',  ( -4.000000000000000000, -2.309401076758512694, -3.433295621305382461 ) ) ;
#10277=ORIENTED_EDGE ( 'NONE', *, *, #14382, .F. ) ;
#10285=DIRECTION ( 'NONE',  ( 1.000000000000000000, 0.000000000000000000, 0.000000000000000000 ) ) ;
#10306=CARTESIAN_POINT ( 'NONE',  ( 2.059999999999998721, 0.000000000000000000, -0.3080913168122742518 ) ) ;
#10312=CARTESIAN_POINT ( 'NONE',  ( -4.000000000000000000, -1.560351142792950618, -0.2242961665059814425 ) ) ;
#10314=AXIS2_PLACEMENT_3D ( 'NONE', #5220, #7490, #6608 ) ;
#10331=FACE_OUTER_BOUND ( 'NONE', #12323, .T. ) ;
#10336=CIRCLE ( 'NONE', #11735, 2.100000000000000089 ) ;
#10339=ORIENTED_EDGE ( 'NONE', *, *, #3606, .T. ) ;
#10340=DIRECTION ( 'NONE',  ( 0.8660254037844379305, 0.5000000000000013323, 0.000000000000000000 ) ) ;
#10366=CARTESIAN_POINT ( 'NONE',  ( -0.1750025118121544265, -4.719839900820635314, -3.469254087858253399 ) ) ;
#10376=ORIENTED_EDGE ( 'NONE', *, *, #6399, .F. ) ;
#10381=FACE_OUTER_BOUND ( 'NONE', #10475, .T. ) ;
#10412=VERTEX_POINT ( 'NONE', #14391 ) ;
#10423=CARTESIAN_POINT ( 'NONE',  ( -1.654252653721913102, -3.663718938583024443, -0.01223254789874440342 ) ) ;
#10438=LINE ( 'NONE', #7032, #1660 ) ;
#10475=EDGE_LOOP ( 'NONE', ( #1757, #4536, #13475, #4911, #4065 ) ) ;
#10483=CARTESIAN_POINT ( 'NONE',  ( 4.000000000000000000, 2.309401076758515803, -0.4999999999999995559 ) ) ;
#10507=CARTESIAN_POINT ( 'NONE',  ( 4.175648173966055587, -2.207990556236547608, -3.469390959564065291 ) ) ;
#10537=CARTESIAN_POINT ( 'NONE',  ( 0.000000000000000000, 0.000000000000000000, 3.469446951953614189E-15 ) ) ;
#10541=CARTESIAN_POINT ( 'NONE',  ( -4.204114297095464359, 1.660363174096617156, -3.602136431857887011 ) ) ;
#10550=CIRCLE ( 'NONE', #9133, 2.499999999999999556 ) ;
#10552=CARTESIAN_POINT ( 'NONE',  ( 4.000000000000000888, -0.8578082829538523635, -3.433262215449808696 ) ) ;
#10556=VERTEX_POINT ( 'NONE', #13794 ) ;
#10584=CARTESIAN_POINT ( 'NONE',  ( 4.236525694536557474, -2.416953475386482530, -3.751298745799839462 ) ) ;
#10598=CARTESIAN_POINT ( 'NONE',  ( -4.175002511812151873, -2.208363329454905877, -3.469254087858246738 ) ) ;
#10621=CARTESIAN_POINT ( 'NONE',  ( 0.6810597143197052450, 4.461075778259290914, -3.598441714920602053 ) ) ;
#10623=CARTESIAN_POINT ( 'NONE',  ( -4.000000000000000000, -0.8232339106130515116, -3.430630286862743183 ) ) ;
#10635=CARTESIAN_POINT ( 'NONE',  ( 4.000000000000000000, -1.700175430507292473, -3.320327275037661785 ) ) ;
#10663=CARTESIAN_POINT ( 'NONE',  ( -3.861362476283256129, -2.629030857716004199, -3.671615880910374941 ) ) ;
#10670=CARTESIAN_POINT ( 'NONE',  ( -4.000000000000000888, 1.563622288139195238, -0.2253451193528307472 ) ) ;
#10688=CARTESIAN_POINT ( 'NONE',  ( -5.384454397937118664, 6.702023979852544604E-16, -5.000000000000000000 ) ) ;
#10694=CARTESIAN_POINT ( 'NONE',  ( 1.287237434362044075, 3.875615274277557809, -3.430618716626812059 ) ) ;
#10696=CARTESIAN_POINT ( 'NONE',  ( -4.211405944401398038, -2.460460786169389902, -3.751298493805494072 ) ) ;
#10705=DIRECTION ( 'NONE',  ( -1.000000000000000000, 0.000000000000000000, 0.000000000000000000 ) ) ;
#10722=EDGE_CURVE ( 'NONE', #992, #740, #3634, .T. ) ;
#10730=CARTESIAN_POINT ( 'NONE',  ( 0.000000000000000000, 0.000000000000000000, 0.000000000000000000 ) ) ;
#10756=CARTESIAN_POINT ( 'NONE',  ( -0.5276280594146446346, 4.314175951381965746, -3.320322319201721495 ) ) ;
#10759=CARTESIAN_POINT ( 'NONE',  ( -4.203934362469166963, -1.640673743454851286, -3.598432614606932756 ) ) ;
#10792=DIRECTION ( 'NONE',  ( -1.000000000000000000, 0.000000000000000000, 0.000000000000000000 ) ) ;
#10793=CARTESIAN_POINT ( 'NONE',  ( -3.264624719419710521E-13, -4.796980096169328966, -3.721999068284310486 ) ) ;
#10801=ORIENTED_EDGE ( 'NONE', *, *, #14231, .T. ) ;
#10802=EDGE_LOOP ( 'NONE', ( #8981, #8765, #2299, #10120, #4842 ) ) ;
#10810=PRODUCT_DEFINITION ( 'UNKNOWN', '', #7362, #6349 ) ;
#10812=ORIENTED_EDGE ( 'NONE', *, *, #88, .T. ) ;
#10813=EDGE_LOOP ( 'NONE', ( #7660, #6210, #1854 ) ) ;
#10838=VERTEX_POINT ( 'NONE', #92 ) ;
#10857=ORIENTED_EDGE ( 'NONE', *, *, #2488, .F. ) ;
#10873=CARTESIAN_POINT ( 'NONE',  ( 0.000000000000000000, 0.000000000000000000, -25.03750572909317285 ) ) ;
#10874=TOROIDAL_SURFACE ( 'NONE', #4514, 5.384454397937118664, 0.5155456020628804703 ) ;
#10875=ORIENTED_EDGE ( 'NONE', *, *, #11528, .F. ) ;
#10931=CARTESIAN_POINT ( 'NONE',  ( -6.473970235329672780E-16, -4.862606272033106691, -3.745885042887442395 ) ) ;
#10943=DIRECTION ( 'NONE',  ( 0.000000000000000000, -1.000000000000000000, 0.000000000000000000 ) ) ;
#10969=VERTEX_POINT ( 'NONE', #8443 ) ;
#10986=EDGE_CURVE ( 'NONE', #12480, #3563, #12227, .T. ) ;
#10995=ORIENTED_EDGE ( 'NONE', *, *, #11684, .T. ) ;
#11009=( NAMED_UNIT ( * ) PLANE_ANGLE_UNIT ( ) SI_UNIT ( $, .RADIAN. ) );
#11018=CARTESIAN_POINT ( 'NONE',  ( 4.101954839143203912, 2.368264730583012234, -3.681130640444374436 ) ) ;
#11020=CARTESIAN_POINT ( 'NONE',  ( -2.000000000000006661, 3.464101615137750834, 0.000000000000000000 ) ) ;
#11026=CARTESIAN_POINT ( 'NONE',  ( -0.6640947660597427138, 4.471078309994878985, -3.602146406945963442 ) ) ;
#11028=FACE_OUTER_BOUND ( 'NONE', #11479, .T. ) ;
#11035=ORIENTED_EDGE ( 'NONE', *, *, #2028, .T. ) ;
#11036=DIRECTION ( 'NONE',  ( 0.000000000000000000, 0.000000000000000000, -1.000000000000000000 ) ) ;
#11042=ORIENTED_EDGE ( 'NONE', *, *, #9090, .T. ) ;
#11049=ORIENTED_EDGE ( 'NONE', *, *, #11342, .T. ) ;
#11068=AXIS2_PLACEMENT_3D ( 'NONE', #13914, #8365, #9407 ) ;
#11098=EDGE_CURVE ( 'NONE', #740, #14327, #3118, .T. ) ;
#11139=CARTESIAN_POINT ( 'NONE',  ( 4.000000000000000000, 2.309401076758515803, -0.4999999999999995559 ) ) ;
#11169=DIRECTION ( 'NONE',  ( 0.000000000000000000, 0.000000000000000000, 1.000000000000000000 ) ) ;
#11172=ADVANCED_FACE ( 'NONE', ( #5138 ), #5935, .T. ) ;
#11179=CARTESIAN_POINT ( 'NONE',  ( -2.712762565639006418, 3.052587955997511759, -3.430618716626627318 ) ) ;
#11194=CARTESIAN_POINT ( 'NONE',  ( -4.211140560182196957, -2.431303136016552013, -3.745885042887436178 ) ) ;
#11195=CARTESIAN_POINT ( 'NONE',  ( 2.000000000000005329, -3.464101615137751722, 0.000000000000000000 ) ) ;
#11208=CARTESIAN_POINT ( 'NONE',  ( 4.000000000000000000, 0.9868501483902631932, -0.09357334158579604100 ) ) ;
#11234=CARTESIAN_POINT ( 'NONE',  ( -1.393927851585477606, 4.043713361053528743, -3.526374918436835149 ) ) ;
#11244=CARTESIAN_POINT ( 'NONE',  ( -2.000000000000006661, 3.464101615137750834, 0.000000000000000000 ) ) ;
#11275=CARTESIAN_POINT ( 'NONE',  ( 3.511755186886750923, -2.826662030176382956, -3.597382984111582083 ) ) ;
#11282=ORIENTED_EDGE ( 'NONE', *, *, #12700, .F. ) ;
#11308=ORIENTED_EDGE ( 'NONE', *, *, #4681, .F. ) ;
#11322=CARTESIAN_POINT ( 'NONE',  ( 4.000000000000000000, -2.309401076758514915, -3.433295621305383349 ) ) ;
#11338=ORIENTED_EDGE ( 'NONE', *, *, #6579, .F. ) ;
#11342=EDGE_CURVE ( 'NONE', #2446, #1880, #2037, .T. ) ;
#11366=DIRECTION ( 'NONE',  ( -0.000000000000000000, -0.000000000000000000, 1.000000000000000000 ) ) ;
#11390=CARTESIAN_POINT ( 'NONE',  ( 4.211399257449709665, -2.459727064652517114, -3.751161691472417736 ) ) ;
#11402=ORIENTED_EDGE ( 'NONE', *, *, #13992, .F. ) ;
#11417=EDGE_CURVE ( 'NONE', #10412, #14577, #6960, .T. ) ;
#11423=CARTESIAN_POINT ( 'NONE',  ( 0.000000000000000000, 0.000000000000000000, 0.000000000000000000 ) ) ;
#11426=ORIENTED_EDGE ( 'NONE', *, *, #3048, .T. ) ;
#11453=ORIENTED_EDGE ( 'NONE', *, *, #6275, .F. ) ;
#11474=DIRECTION ( 'NONE',  ( -1.000000000000000000, 0.000000000000000000, 0.000000000000000000 ) ) ;
#11479=EDGE_LOOP ( 'NONE', ( #6577, #10339, #5294, #12130, #2482, #5428, #3168 ) ) ;
#11504=CARTESIAN_POINT ( 'NONE',  ( 4.000000000000003553, -2.309401076758513138, -3.504271511727127031 ) ) ;
#11508=ADVANCED_FACE ( 'NONE', ( #12676 ), #3599, .T. ) ;
#11511=VECTOR ( 'NONE', #13151, 1000.000000000000227 ) ;
#11521=ORIENTED_EDGE ( 'NONE', *, *, #4982, .F. ) ;
#11528=EDGE_CURVE ( 'NONE', #6453, #14577, #3457, .T. ) ;
#11529=B_SPLINE_CURVE_WITH_KNOTS ( 'NONE', 3,
 ( #6161, #14057, #9404, #9264, #7035, #7333, #10663, #13995 ),
 .UNSPECIFIED., .F., .F.,
 ( 4, 2, 2, 4 ),
 ( 0.000000000000000000, 0.002450665683189818828, 0.003675998524784728459, 0.004901331366379638524 ),
 .UNSPECIFIED. ) ;
#11532=ORIENTED_EDGE ( 'NONE', *, *, #4397, .T. ) ;
#11539=CARTESIAN_POINT ( 'NONE',  ( -4.154094228333542915, 2.398367420968061658, -3.721909803043254694 ) ) ;
#11555=DIRECTION ( 'NONE',  ( -0.000000000000000000, -0.000000000000000000, 1.000000000000000000 ) ) ;
#11573=CARTESIAN_POINT ( 'NONE',  ( 3.472371940585993855, 2.614027278893175321, -3.320322319201766792 ) ) ;
#11598=ORIENTED_EDGE ( 'NONE', *, *, #6809, .F. ) ;
#11622=CIRCLE ( 'NONE', #13516, 4.000000000000000000 ) ;
#11624=DIRECTION ( 'NONE',  ( 0.000000000000000000, 0.000000000000000000, 1.000000000000000000 ) ) ;
#11626=DIRECTION ( 'NONE',  ( 1.000000000000000000, 0.000000000000000000, 0.000000000000000000 ) ) ;
#11631=CARTESIAN_POINT ( 'NONE',  ( -4.197393957002303999, -7.773935952363655451E-14, -3.503767560748929810 ) ) ;
#11646=CARTESIAN_POINT ( 'NONE',  ( 4.197393957002303999, 0.8151795401431359833, -3.503767560748935139 ) ) ;
#11653=CARTESIAN_POINT ( 'NONE',  ( -4.211140560182196957, 2.431303136016537803, -3.745885042887433514 ) ) ;
#11654=EDGE_CURVE ( 'NONE', #14327, #2290, #6069, .T. ) ;
#11655=DIRECTION ( 'NONE',  ( -1.000000000000000000, 0.000000000000000000, 0.000000000000000000 ) ) ;
#11669=B_SPLINE_CURVE_WITH_KNOTS ( 'NONE', 3,
 ( #1947, #5200, #9627, #9777, #6297 ),
 .UNSPECIFIED., .F., .F.,
 ( 4, 1, 4 ),
 ( 0.000000000000000000, 0.002309401076758505356, 0.004618802153517010713 ),
 .UNSPECIFIED. ) ;
#11683=CARTESIAN_POINT ( 'NONE',  ( -4.000000000000000000, 0.1981133338132459731, 2.096406544454392723E-17 ) ) ;
#11684=EDGE_CURVE ( 'NONE', #6458, #8478, #9726, .T. ) ;
#11693=CARTESIAN_POINT ( 'NONE',  ( 0.000000000000000000, 0.000000000000000000, -4.694516984716113228 ) ) ;
#11695=ORIENTED_EDGE ( 'NONE', *, *, #4385, .F. ) ;
#11708=CARTESIAN_POINT ( 'NONE',  ( 4.140404888673277384, 2.228338276487440428, -3.686887068327033390 ) ) ;
#11712=ORIENTED_EDGE ( 'NONE', *, *, #3460, .T. ) ;
#11720=CARTESIAN_POINT ( 'NONE',  ( 4.211405965630455661, 2.460463115436283932, -3.751298928144577882 ) ) ;
#11733=CARTESIAN_POINT ( 'NONE',  ( 2.000000000000008882, 3.464101615137749945, 0.000000000000000000 ) ) ;
#11735=AXIS2_PLACEMENT_3D ( 'NONE', #5339, #890, #6590 ) ;
#11763=DIRECTION ( 'NONE',  ( -1.000000000000000000, 0.000000000000000000, 0.000000000000000000 ) ) ;
#11766=CIRCLE ( 'NONE', #8005, 5.384454397937118664 ) ;
#11779=DIRECTION ( 'NONE',  ( -0.000000000000000000, -0.000000000000000000, 1.000000000000000000 ) ) ;
#11805=DIRECTION ( 'NONE',  ( -0.000000000000000000, 0.000000000000000000, -1.000000000000000000 ) ) ;
#11825=AXIS2_PLACEMENT_3D ( 'NONE', #11423, #43, #9001 ) ;
#11837=CARTESIAN_POINT ( 'NONE',  ( -4.000000000000000000, 2.309401076758498483, -0.4999999999999927280 ) ) ;
#11842=CARTESIAN_POINT ( 'NONE',  ( 0.000000000000000000, 0.000000000000000000, -5.000000000000000000 ) ) ;
#11846=CARTESIAN_POINT ( 'NONE',  ( -2.836893136758495970, -3.208949435745868328, -3.505054077164885484 ) ) ;
#11877=CARTESIAN_POINT ( 'NONE',  ( 0.000000000000000000, 0.000000000000000000, 0.000000000000000000 ) ) ;
#11888=PLANE ( 'NONE',  #10083 ) ;
#11898=CARTESIAN_POINT ( 'NONE',  ( 1.411581201560190495E-15, 4.862606272033091592, -3.745885042887436622 ) ) ;
#11904=EDGE_CURVE ( 'NONE', #740, #9530, #4670, .T. ) ;
#11907=ADVANCED_FACE ( 'NONE', ( #12659 ), #14595, .T. ) ;
#11923=CARTESIAN_POINT ( 'NONE',  ( -3.679171394226034675, -2.494631558665844739, -0.3503314178412558211 ) ) ;
#11925=CARTESIAN_POINT ( 'NONE',  ( -4.000000000000000000, 2.511478553582031203, -3.469254451724764543 ) ) ;
#11937=CARTESIAN_POINT ( 'NONE',  ( -4.101948962586059899, -2.368261337751176754, -3.681124513963741851 ) ) ;
#11949=VERTEX_POINT ( 'NONE', #13783 ) ;
#11955=ADVANCED_FACE ( 'NONE', ( #10381 ), #8017, .T. ) ;
#11959=VERTEX_POINT ( 'NONE', #11631 ) ;
#11963=CARTESIAN_POINT ( 'NONE',  ( 4.000000000000000000, 0.3987449864460005378, -0.01220643443059817035 ) ) ;
#11969=ORIENTED_EDGE ( 'NONE', *, *, #13987, .T. ) ;
#12003=DIRECTION ( 'NONE',  ( 0.000000000000000000, 0.000000000000000000, 1.000000000000000000 ) ) ;
#12027=SHAPE_DEFINITION_REPRESENTATION ( #5807, #6779 ) ;
#12043=ADVANCED_FACE ( 'NONE', ( #5077 ), #9572, .F. ) ;
#12065=DIRECTION ( 'NONE',  ( -0.000000000000000000, -0.000000000000000000, 1.000000000000000000 ) ) ;
#12116=CARTESIAN_POINT ( 'NONE',  ( 3.383466608491643077E-15, 4.736522675502341073, -3.681124513963742739 ) ) ;
#12118=( LENGTH_UNIT ( ) NAMED_UNIT ( * ) SI_UNIT ( .MILLI., .METRE. ) );
#12127=( BOUNDED_SURFACE ( )  B_SPLINE_SURFACE ( 3, 2, ( 
 ( #10366, #307, #13832 ),
 ( #12945, #2755, #7192 ),
 ( #13997, #4843, #8215 ),
 ( #9336, #1511, #2835 ),
 ( #7338, #1653, #3885 ),
 ( #10507, #13767, #10584 ) ),
 .UNSPECIFIED., .F., .F., .T. ) 
 B_SPLINE_SURFACE_WITH_KNOTS ( ( 4, 2, 4 ),
 ( 3, 3 ),
 ( 0.02032853247518126918, 0.02278863295364821906, 0.02524873343211517240 ),
 ( 0.000000000000000000, 1.000000000000000000 ),
 .UNSPECIFIED. ) 
 GEOMETRIC_REPRESENTATION_ITEM ( )  RATIONAL_B_SPLINE_SURFACE ( (
 ( 1.000000000000000000, 0.8047781615896837382, 1.000000000000000000),
 ( 1.000000000000000000, 0.8123767586289252218, 1.000000000000000000),
 ( 1.000000000000000000, 0.8190662415564388121, 1.000000000000000000),
 ( 1.000000000000000000, 0.8192361015669026303, 1.000000000000000000),
 ( 1.000000000000000000, 0.8126135807103900266, 1.000000000000000000),
 ( 1.000000000000000000, 0.8047712338318593339, 1.000000000000000000) ) ) 
 REPRESENTATION_ITEM ( '' )  SURFACE ( )  );
#12130=ORIENTED_EDGE ( 'NONE', *, *, #3460, .F. ) ;
#12147=ADVANCED_FACE ( 'NONE', ( #11028 ), #7860, .T. ) ;
#12150=DIRECTION ( 'NONE',  ( 1.000000000000000000, 0.000000000000000000, 0.000000000000000000 ) ) ;
#12178=ORIENTED_EDGE ( 'NONE', *, *, #9510, .F. ) ;
#12181=CYLINDRICAL_SURFACE ( 'NONE', #670, 2.100000000000000089 ) ;
#12190=CARTESIAN_POINT ( 'NONE',  ( 4.000000000000000000, -2.511475576507276042, -3.469253905236643565 ) ) ;
#12227=B_SPLINE_CURVE_WITH_KNOTS ( 'NONE', 3,
 ( #477, #2636, #316, #5006, #14007, #13929, #2848, #4854 ),
 .UNSPECIFIED., .F., .F.,
 ( 4, 2, 2, 4 ),
 ( 7.780516681398759253E-20, 0.002450665683189819696, 0.003675998524784729327, 0.004901331366379639391 ),
 .UNSPECIFIED. ) ;
#12230=VECTOR ( 'NONE', #10115, 1000.000000000000227 ) ;
#12249=AXIS2_PLACEMENT_3D ( 'NONE', #5217, #1740, #5289 ) ;
#12277=CARTESIAN_POINT ( 'NONE',  ( -6.259644161404860030E-16, -4.618802153517027165, -3.433295621305388234 ) ) ;
#12291=MANIFOLD_SOLID_BREP ( 'EndChamfer', #9748 ) ;
#12304=DIRECTION ( 'NONE',  ( -0.5000000000000016653, 0.8660254037844378194, 0.000000000000000000 ) ) ;
#12323=EDGE_LOOP ( 'NONE', ( #3673, #7458, #8521, #6689 ) ) ;
#12343=CARTESIAN_POINT ( 'NONE',  ( 4.207491450040567571, -2.029819825146485179, -3.671670828759567407 ) ) ;
#12352=CARTESIAN_POINT ( 'NONE',  ( 0.6666666666666658525, -4.233901974057276085, -3.300726591567086476 ) ) ;
#12357=ORIENTED_EDGE ( 'NONE', *, *, #5278, .F. ) ;
#12359=EDGE_CURVE ( 'NONE', #1880, #6883, #11529, .T. ) ;
#12362=DIRECTION ( 'NONE',  ( -0.000000000000000000, -0.000000000000000000, 1.000000000000000000 ) ) ;
#12368=DIRECTION ( 'NONE',  ( -0.8660254037844373753, 0.5000000000000021094, 0.000000000000000000 ) ) ;
#12394=CARTESIAN_POINT ( 'NONE',  ( -4.000000000000000000, -2.309401076758512694, -3.433295621305382461 ) ) ;
#12405=CARTESIAN_POINT ( 'NONE',  ( 4.197393957002303999, 7.772902908466098641E-14, -3.503767560748929810 ) ) ;
#12408=EDGE_CURVE ( 'NONE', #7500, #4931, #10336, .T. ) ;
#12435=CIRCLE ( 'NONE', #3022, 0.5155456020628804703 ) ;
#12459=EDGE_LOOP ( 'NONE', ( #7380, #6231, #7339, #7537, #12679 ) ) ;
#12469=AXIS2_PLACEMENT_3D ( 'NONE', #14300, #6486, #12150 ) ;
#12480=VERTEX_POINT ( 'NONE', #11898 ) ;
#12486=VECTOR ( 'NONE', #14491, 1000.000000000000000 ) ;
#12532=COLOUR_RGB ( '',1.000000000000000000, 0.9490196078431372140, 0.9098039215686274384 ) ;
#12542=CARTESIAN_POINT ( 'NONE',  ( 0.000000000000000000, 0.000000000000000000, -5.000000000000000000 ) ) ;
#12572=CARTESIAN_POINT ( 'NONE',  ( 4.204115023516791005, -1.660442669500199919, -3.602151381774560068 ) ) ;
#12611=EDGE_LOOP ( 'NONE', ( #8195, #1827, #8313 ) ) ;
#12647=CARTESIAN_POINT ( 'NONE',  ( -4.000000000000000000, 2.309401076758498483, -3.433295621305379353 ) ) ;
#12658=CARTESIAN_POINT ( 'NONE',  ( -1.287237434361707233, -3.875615274277397937, -3.430618716626816500 ) ) ;
#12659=FACE_OUTER_BOUND ( 'NONE', #1203, .T. ) ;
#12662=CIRCLE ( 'NONE', #9603, 2.500000000000000888 ) ;
#12676=FACE_OUTER_BOUND ( 'NONE', #12611, .T. ) ;
#12679=ORIENTED_EDGE ( 'NONE', *, *, #6128, .F. ) ;
#12682=DIRECTION ( 'NONE',  ( 1.000000000000000000, 0.000000000000000000, 0.000000000000000000 ) ) ;
#12692=B_SPLINE_CURVE_WITH_KNOTS ( 'NONE', 3,
 ( #8183, #3854, #9237, #13657, #5982, #10483 ),
 .UNSPECIFIED., .F., .F.,
 ( 4, 2, 4 ),
 ( 0.002365888236227995517, 0.003551327329835084114, 0.004736766423442172712 ),
 .UNSPECIFIED. ) ;
#12700=EDGE_CURVE ( 'NONE', #9530, #14327, #3467, .T. ) ;
#12708=ORIENTED_EDGE ( 'NONE', *, *, #2609, .F. ) ;
#12717=CARTESIAN_POINT ( 'NONE',  ( -1.149515148933674504E-15, -4.647091401871393579, -3.572172305156879890 ) ) ;
#12731=VECTOR ( 'NONE', #11624, 1000.000000000000000 ) ;
#12737=ORIENTED_EDGE ( 'NONE', *, *, #8983, .F. ) ;
#12755=CARTESIAN_POINT ( 'NONE',  ( 3.333333333333332593, 2.694301256218250007, -3.300726591567078483 ) ) ;
#12761=CARTESIAN_POINT ( 'NONE',  ( -0.1756481739660520902, 4.720212674038980261, -3.469390959564065291 ) ) ;
#12780=CARTESIAN_POINT ( 'NONE',  ( -2.000000000000007550, -3.464101615137749945, 0.000000000000000000 ) ) ;
#12835=FACE_BOUND ( 'NONE', #1082, .T. ) ;
#12845=CARTESIAN_POINT ( 'NONE',  ( 4.197478902586992966, -0.8524102783748346290, -3.505063281295504041 ) ) ;
#12849=UNCERTAINTY_MEASURE_WITH_UNIT (LENGTH_MEASURE( 1.000000000000000082E-05 ), #12118, 'distance_accuracy_value', 'NONE');
#12851=ORIENTED_EDGE ( 'NONE', *, *, #14382, .T. ) ;
#12869=LINE ( 'NONE', #1568, #6771 ) ;
#12884=CARTESIAN_POINT ( 'NONE',  ( 0.000000000000000000, 0.000000000000000000, 0.000000000000000000 ) ) ;
#12886=ORIENTED_EDGE ( 'NONE', *, *, #7774, .F. ) ;
#12897=FACE_OUTER_BOUND ( 'NONE', #658, .T. ) ;
#12918=FACE_OUTER_BOUND ( 'NONE', #6473, .T. ) ;
#12941=DIRECTION ( 'NONE',  ( 0.000000000000000000, 0.000000000000000000, 1.000000000000000000 ) ) ;
#12945=CARTESIAN_POINT ( 'NONE',  ( 0.5276280594147412240, -4.314175951381924889, -3.320322319201654881 ) ) ;
#12998=VECTOR ( 'NONE', #2680, 1000.000000000000000 ) ;
#13016=UNCERTAINTY_MEASURE_WITH_UNIT (LENGTH_MEASURE( 1.000000000000000082E-05 ), #2393, 'distance_accuracy_value', 'NONE');
#13022=CARTESIAN_POINT ( 'NONE',  ( -2.500000000000000888, 0.000000000000000000, -4.974599999999998801 ) ) ;
#13031=EDGE_LOOP ( 'NONE', ( #4150, #1441, #12178, #560 ) ) ;
#13033=CARTESIAN_POINT ( 'NONE',  ( -4.000000000000000000, 0.3987449864459974846, -0.01220643443059782861 ) ) ;
#13052=ORIENTED_EDGE ( 'NONE', *, *, #11098, .F. ) ;
#13072=CARTESIAN_POINT ( 'NONE',  ( -4.211140560182196957, -2.431303136016552013, -3.745885042887436178 ) ) ;
#13074=ORIENTED_EDGE ( 'NONE', *, *, #6809, .T. ) ;
#13093=DIRECTION ( 'NONE',  ( 0.000000000000000000, 0.000000000000000000, -1.000000000000000000 ) ) ;
#13094=CARTESIAN_POINT ( 'NONE',  ( 1.567478505476134606E-15, 4.618802153517012066, -3.433295621305382905 ) ) ;
#13113=DIRECTION ( 'NONE',  ( 0.000000000000000000, 0.000000000000000000, -1.000000000000000000 ) ) ;
#13151=DIRECTION ( 'NONE',  ( -0.9396926207859138680, 0.000000000000000000, -0.3420201433256536139 ) ) ;
#13162=( NAMED_UNIT ( * ) SI_UNIT ( $, .STERADIAN. ) SOLID_ANGLE_UNIT ( ) );
#13206=DIRECTION ( 'NONE',  ( -0.8660254037844377084, -0.5000000000000015543, 0.000000000000000000 ) ) ;
#13231=AXIS2_PLACEMENT_3D ( 'NONE', #1070, #14517, #4404 ) ;
#13263=ORIENTED_EDGE ( 'NONE', *, *, #10722, .T. ) ;
#13269=AXIS2_PLACEMENT_3D ( 'NONE', #14072, #3958, #14147 ) ;
#13330=CARTESIAN_POINT ( 'NONE',  ( 0.000000000000000000, 0.000000000000000000, 0.000000000000000000 ) ) ;
#13335=ADVANCED_FACE ( 'NONE', ( #8505 ), #1639, .F. ) ;
#13354=LINE ( 'NONE', #2208, #6150 ) ;
#13373=ADVANCED_FACE ( 'NONE', ( #449 ), #2333, .T. ) ;
#13379=DIRECTION ( 'NONE',  ( -1.000000000000000000, 0.000000000000000000, 0.000000000000000000 ) ) ;
#13386=CARTESIAN_POINT ( 'NONE',  ( 0.02448733951239481094, 4.877042772274728044, -3.751161874094022242 ) ) ;
#13416=ORIENTED_EDGE ( 'NONE', *, *, #7715, .T. ) ;
#13418=EDGE_CURVE ( 'NONE', #9996, #2290, #8691, .T. ) ;
#13434=DIRECTION ( 'NONE',  ( -0.8191520442889875797, 1.003171929053519570E-16, 0.5735764363510522656 ) ) ;
#13464=CARTESIAN_POINT ( 'NONE',  ( 4.000000000001088907, 1.658577278524410170, -3.531553309554541720 ) ) ;
#13472=CARTESIAN_POINT ( 'NONE',  ( -1.317756351988340180, 3.857995168970202116, -0.04852650426601388955 ) ) ;
#13475=ORIENTED_EDGE ( 'NONE', *, *, #13418, .T. ) ;
#13516=AXIS2_PLACEMENT_3D ( 'NONE', #8358, #7182, #10792 ) ;
#13525=ORIENTED_EDGE ( 'NONE', *, *, #7288, .T. ) ;
#13537=CARTESIAN_POINT ( 'NONE',  ( -4.197393957002303999, -7.773935952363655451E-14, -3.503767560748929810 ) ) ;
#13543=CARTESIAN_POINT ( 'NONE',  ( 1.734723475976807094E-15, 4.618802153517012954, -0.4999999999999995559 ) ) ;
#13557=CARTESIAN_POINT ( 'NONE',  ( 1.317756351988342622, -3.857995168970215438, -0.04852650426602527628 ) ) ;
#13565=CARTESIAN_POINT ( 'NONE',  ( 0.3461262719736147297, -4.658553426539303821, -3.671615880910379381 ) ) ;
#13572=CARTESIAN_POINT ( 'NONE',  ( 0.000000000000000000, 0.000000000000000000, -5.000000000000000000 ) ) ;
#13590=CARTESIAN_POINT ( 'NONE',  ( -3.999999999999999112, 1.539600717838996324, -3.300726591567078039 ) ) ;
#13618=CONICAL_SURFACE ( 'NONE', #10314, 2.059999999999998721, 0.9599310885968738161 ) ;
#13625=CARTESIAN_POINT ( 'NONE',  ( -4.203833317240879275, -1.627343821129593859, -3.597273115243890818 ) ) ;
#13626=DIRECTION ( 'NONE',  ( 0.5000000000000022204, 0.8660254037844374864, -0.000000000000000000 ) ) ;
#13654=CARTESIAN_POINT ( 'NONE',  ( 4.154306624730763176, -2.398490048084970461, -3.721999068284303824 ) ) ;
#13657=CARTESIAN_POINT ( 'NONE',  ( 3.349226789952652439, 2.685125164760731487, -0.2236248678334773199 ) ) ;
#13673=ORIENTED_EDGE ( 'NONE', *, *, #6621, .F. ) ;
#13674=CARTESIAN_POINT ( 'NONE',  ( 4.000000000000000888, 1.539600717838996990, -3.300726591567079815 ) ) ;
#13691=EDGE_CURVE ( 'NONE', #6877, #10838, #4566, .T. ) ;
#13697=ORIENTED_EDGE ( 'NONE', *, *, #1667, .F. ) ;
#13715=LINE ( 'NONE', #10306, #10121 ) ;
#13733=DIRECTION ( 'NONE',  ( 1.000000000000000000, 0.000000000000000000, 0.000000000000000000 ) ) ;
#13755=CARTESIAN_POINT ( 'NONE',  ( 4.211140560182196957, -2.431303136016555122, -3.745885042887436622 ) ) ;
#13767=CARTESIAN_POINT ( 'NONE',  ( 4.141042297810615835, -2.227970268150433863, -3.687027686973623819 ) ) ;
#13783=CARTESIAN_POINT ( 'NONE',  ( 1.734723475976807094E-15, 4.618802153517012954, -0.4999999999999995559 ) ) ;
#13785=CARTESIAN_POINT ( 'NONE',  ( 0.000000000000000000, 0.000000000000000000, -5.000000000000000000 ) ) ;
#13794=CARTESIAN_POINT ( 'NONE',  ( 5.560781378645575757, 0.000000000000000000, -4.000000000000000000 ) ) ;
#13798=CARTESIAN_POINT ( 'NONE',  ( -0.02511973781850462134, 4.877415612947412882, -3.751298745799839462 ) ) ;
#13832=CARTESIAN_POINT ( 'NONE',  ( -0.02448733951239248641, -4.877042772274742255, -3.751161874094027571 ) ) ;
#13842=EDGE_CURVE ( 'NONE', #14327, #10969, #3538, .T. ) ;
#13844=CARTESIAN_POINT ( 'NONE',  ( -4.235886605889389145, -2.417314728048544303, -3.751161874094020909 ) ) ;
#13848=AXIS2_PLACEMENT_3D ( 'NONE', #11842, #1518, #11626 ) ;
#13863=DIRECTION ( 'NONE',  ( 1.000000000000000000, 0.000000000000000000, 0.000000000000000000 ) ) ;
#13869=ADVANCED_FACE ( 'NONE', ( #3147 ), #2345, .F. ) ;
#13877=CARTESIAN_POINT ( 'NONE',  ( 4.101954839143203912, -2.368264730583031330, -3.681130640444377988 ) ) ;
#13914=CARTESIAN_POINT ( 'NONE',  ( 0.000000000000000000, 0.000000000000000000, -4.000000000000000000 ) ) ;
#13920=AXIS2_PLACEMENT_3D ( 'NONE', #14613, #10185, #3688 ) ;
#13929=CARTESIAN_POINT ( 'NONE',  ( 3.510273485745307731, 2.827716139362654424, -3.610536846335885564 ) ) ;
#13950=CARTESIAN_POINT ( 'NONE',  ( 4.000000000000000000, -2.309401076758516691, -0.4999999999999995559 ) ) ;
#13953=CARTESIAN_POINT ( 'NONE',  ( -4.000000000000000000, -0.8382240730041925492, -3.220610619767135141 ) ) ;
#13979=CARTESIAN_POINT ( 'NONE',  ( 4.000000000000000000, -1.084202172485504434E-14, -3.142992957459231906 ) ) ;
#13987=EDGE_CURVE ( 'NONE', #4931, #7500, #14379, .T. ) ;
#13988=AXIS2_PLACEMENT_3D ( 'NONE', #4158, #10943, #6516 ) ;
#13991=CARTESIAN_POINT ( 'NONE',  ( 0.000000000000000000, 0.000000000000000000, 0.000000000000000000 ) ) ;
#13992=EDGE_CURVE ( 'NONE', #11949, #3419, #5336, .T. ) ;
#13995=CARTESIAN_POINT ( 'NONE',  ( -4.211140560182196957, -2.431303136016552013, -3.745885042887436178 ) ) ;
#13997=CARTESIAN_POINT ( 'NONE',  ( 1.243802165048773611, -3.900692638707475624, -3.223146290109810241 ) ) ;
#14000=( GEOMETRIC_REPRESENTATION_CONTEXT ( 3 ) GLOBAL_UNCERTAINTY_ASSIGNED_CONTEXT ( ( #13016 ) ) GLOBAL_UNIT_ASSIGNED_CONTEXT ( ( #2393, #2238, #10144 ) ) REPRESENTATION_CONTEXT ( 'NONE', 'WORKASPACE' ) );
#14007=CARTESIAN_POINT ( 'NONE',  ( 2.804994570502171047, 3.229033611042449792, -3.526374918436834704 ) ) ;
#14022=CARTESIAN_POINT ( 'NONE',  ( 2.836893136758676270, 3.208949435745843903, -3.505054077164911241 ) ) ;
#14025=CARTESIAN_POINT ( 'NONE',  ( -4.000000000000000000, 1.677772373332757194, -3.535253723897187506 ) ) ;
#14051=ORIENTED_EDGE ( 'NONE', *, *, #9158, .T. ) ;
#14057=CARTESIAN_POINT ( 'NONE',  ( -0.6920835326022555245, -4.454600218803899558, -3.597382984111586079 ) ) ;
#14060=EDGE_LOOP ( 'NONE', ( #2178, #6654, #5980, #7004, #3353 ) ) ;
#14071=CARTESIAN_POINT ( 'NONE',  ( -3.540020015735593439, -2.810662092924100630, -3.602146406945814672 ) ) ;
#14072=CARTESIAN_POINT ( 'NONE',  ( 0.000000000000000000, 0.000000000000000000, -25.03750572909317285 ) ) ;
#14085=CARTESIAN_POINT ( 'NONE',  ( -2.000000000000007550, -3.464101615137749945, 0.000000000000000000 ) ) ;
#14119=CARTESIAN_POINT ( 'NONE',  ( -6.473970235329672780E-16, -4.862606272033106691, -3.745885042887442395 ) ) ;
#14123=CARTESIAN_POINT ( 'NONE',  ( 1.567478505476134803E-15, 4.618802153517012954, -3.504269196027872457 ) ) ;
#14125=ORIENTED_EDGE ( 'NONE', *, *, #11342, .F. ) ;
#14141=EDGE_CURVE ( 'NONE', #10969, #5056, #7068, .T. ) ;
#14146=CARTESIAN_POINT ( 'NONE',  ( 0.02511973781850649831, -4.877415612947427981, -3.751298745799844792 ) ) ;
#14147=DIRECTION ( 'NONE',  ( 1.000000000000000000, 0.000000000000000000, 0.000000000000000000 ) ) ;
#14167=AXIS2_PLACEMENT_3D ( 'NONE', #7409, #2912, #1857 ) ;
#14207=( LENGTH_UNIT ( ) NAMED_UNIT ( * ) SI_UNIT ( .MILLI., .METRE. ) );
#14217=CARTESIAN_POINT ( 'NONE',  ( 1.567478505476134606E-15, 4.618802153517012066, -5.000000000000000000 ) ) ;
#14231=EDGE_CURVE ( 'NONE', #3145, #992, #10438, .T. ) ;
#14244=ORIENTED_EDGE ( 'NONE', *, *, #88, .F. ) ;
#14266=ORIENTED_EDGE ( 'NONE', *, *, #10253, .T. ) ;
#14274=PRESENTATION_STYLE_ASSIGNMENT (( #7636 ) ) ;
#14287=DIRECTION ( 'NONE',  ( 1.000000000000000000, 0.000000000000000000, 0.000000000000000000 ) ) ;
#14300=CARTESIAN_POINT ( 'NONE',  ( 0.000000000000000000, 0.000000000000000000, -4.484454397937119197 ) ) ;
#14302=DIRECTION ( 'NONE',  ( 0.000000000000000000, 0.000000000000000000, 1.000000000000000000 ) ) ;
#14327=VERTEX_POINT ( 'NONE', #7329 ) ;
#14345=ORIENTED_EDGE ( 'NONE', *, *, #5863, .F. ) ;
#14360=CARTESIAN_POINT ( 'NONE',  ( 4.000000000000000000, 2.309401076758497151, -3.433295621305379353 ) ) ;
#14379=CIRCLE ( 'NONE', #2601, 2.100000000000000089 ) ;
#14382=EDGE_CURVE ( 'NONE', #7674, #8837, #8733, .T. ) ;
#14391=CARTESIAN_POINT ( 'NONE',  ( 4.000000000000000000, 0.000000000000000000, 0.000000000000000000 ) ) ;
#14429=STYLED_ITEM ( 'NONE', ( #14274 ), #7024 ) ;
#14431=CARTESIAN_POINT ( 'NONE',  ( 4.000000000000000000, 2.309401076758497151, -3.433295621305379353 ) ) ;
#14453=AXIS2_PLACEMENT_3D ( 'NONE', #6701, #13626, #12368 ) ;
#14455=CARTESIAN_POINT ( 'NONE',  ( 2.345747346278113987, -3.264484291692503870, -0.01223254789874484924 ) ) ;
#14468=CARTESIAN_POINT ( 'NONE',  ( 4.000000000000000000, 0.1981133338132474442, 2.382280164152719704E-17 ) ) ;
#14490=ADVANCED_FACE ( 'NONE', ( #4731 ), #4502, .T. ) ;
#14491=DIRECTION ( 'NONE',  ( 0.000000000000000000, 0.000000000000000000, 1.000000000000000000 ) ) ;
#14494=CARTESIAN_POINT ( 'NONE',  ( -0.6666666666666651864, 4.233901974057260098, -3.300726591567081147 ) ) ;
#14517=DIRECTION ( 'NONE',  ( -0.000000000000000000, -0.000000000000000000, 1.000000000000000000 ) ) ;
#14545=AXIS2_PLACEMENT_3D ( 'NONE', #2543, #1449, #163 ) ;
#14562=CARTESIAN_POINT ( 'NONE',  ( 4.000000000000000000, 2.309401076758497151, -5.000000000000000000 ) ) ;
#14577=VERTEX_POINT ( 'NONE', #1754 ) ;
#14595=PLANE ( 'NONE',  #14453 ) ;
#14613=CARTESIAN_POINT ( 'NONE',  ( 0.000000000000000000, 0.000000000000000000, -4.000000000000000000 ) ) ;
#14675=COLOUR_RGB('Black',0.12,0.14,0.17);
#14676=FILL_AREA_STYLE_COLOUR('',#14675);
#14677=FILL_AREA_STYLE('',(#14676));
#14678=SURFACE_STYLE_FILL_AREA(#14677);
#14679=SURFACE_SIDE_STYLE('',(#14678));
#14680=SURFACE_STYLE_USAGE(.BOTH.,#14679);
#14681=PRESENTATION_STYLE_ASSIGNMENT((#14680));
ENDSEC;
END-ISO-10303-21;
